ISO-10303-21;
HEADER;
FILE_DESCRIPTION (('STEP AP214'),
    '1' );
FILE_NAME ('Hex Bolt.step',
    '2026-10-23T18:01:19',
    ( '' ),
    ( '' ),
    'SwSTEP 2.0',
    'SolidWorks 2025',
    '' );
FILE_SCHEMA (( 'AUTOMOTIVE_DESIGN' ));
ENDSEC;

DATA;
#35=CARTESIAN_POINT ( 'NONE',  ( 0.4192535942842503527, 1.577705975193650412, 0.03573697939582392430 ) ) ;
#39=VERTEX_POINT ( 'NONE', #10557 ) ;
#49=DIRECTION ( 'NONE',  ( 0.000000000000000000, 0.000000000000000000, -1.000000000000000000 ) ) ;
#94=LINE ( 'NONE', #8250, #10804 ) ;
#96=AXIS2_PLACEMENT_3D ( 'NONE', #10060, #3097, #1937 ) ;
#119=CARTESIAN_POINT ( 'NONE',  ( -0.09057123220595257596, 1.599173898159329976, -0.3809527529760086129 ) ) ;
#154=CARTESIAN_POINT ( 'NONE',  ( -0.4349147617188414694, 0.7512260236060024354, -0.008611041693271251005 ) ) ;
#155=ORIENTED_EDGE ( 'NONE', *, *, #13397, .T. ) ;
#158=DIRECTION ( 'NONE',  ( 1.000000000000000000, 0.000000000000000000, 0.000000000000000000 ) ) ;
#177=ORIENTED_EDGE ( 'NONE', *, *, #5280, .F. ) ;
#194=CIRCLE ( 'NONE', #13862, 0.4349999999999999978 ) ;
#195=CARTESIAN_POINT ( 'NONE',  ( -0.1702285915635917690, 1.581112972951822293, -0.3809527529760087239 ) ) ;
#231=CARTESIAN_POINT ( 'NONE',  ( -0.2846118995245673911, 1.599166939805956256, 0.2689432355367775695 ) ) ;
#246=ORIENTED_EDGE ( 'NONE', *, *, #3419, .T. ) ;
#322=DIRECTION ( 'NONE',  ( -0.000000000000000000, -1.000000000000000000, -0.000000000000000000 ) ) ;
#358=VECTOR ( 'NONE', #10511, 39.37007874015748143 ) ;
#383=EDGE_CURVE ( 'NONE', #2919, #710, #5448, .T. ) ;
#385=CIRCLE ( 'NONE', #8720, 0.4349999999999999978 ) ;
#392=VERTEX_POINT ( 'NONE', #12587 ) ;
#420=CIRCLE ( 'NONE', #5332, 0.4849999999999999312 ) ;
#434=DIRECTION ( 'NONE',  ( 0.000000000000000000, 0.000000000000000000, 1.000000000000000000 ) ) ;
#462=DIRECTION ( 'NONE',  ( 0.000000000000000000, 0.000000000000000000, -1.000000000000000000 ) ) ;
#476=ORIENTED_EDGE ( 'NONE', *, *, #8664, .T. ) ;
#480=CARTESIAN_POINT ( 'NONE',  ( 0.01817859877509219249, 1.603284996591855194, 0.3809527529760087239 ) ) ;
#507=LENGTH_MEASURE_WITH_UNIT ( LENGTH_MEASURE( 0.02539999999999999897 ), #1669 );
#519=EDGE_CURVE ( 'NONE', #6687, #3130, #2785, .T. ) ;
#525=CARTESIAN_POINT ( 'NONE',  ( -0.2324505233676816274, 1.569549437900772393, 0.3592893892332145733 ) ) ;
#558=AXIS2_PLACEMENT_3D ( 'NONE', #7883, #12612, #2053 ) ;
#571=CARTESIAN_POINT ( 'NONE',  ( -0.3930894239865136974, 1.593697031032158318, -0.08105465168939116061 ) ) ;
#632=CARTESIAN_POINT ( 'NONE',  ( 0.2285544654201319137, 1.564824237736521129, -0.3660375595476001442 ) ) ;
#655=VECTOR ( 'NONE', #7061, 39.37007874015748143 ) ;
#676=EDGE_LOOP ( 'NONE', ( #8791, #5902, #11091, #7043 ) ) ;
#710=VERTEX_POINT ( 'NONE', #11650 ) ;
#713=CARTESIAN_POINT ( 'NONE',  ( 0.2667400994511441303, 1.593697031032149880, -0.2998981012866574480 ) ) ;
#757=AXIS2_PLACEMENT_3D ( 'NONE', #6640, #6711, #10307 ) ;
#786=DIRECTION ( 'NONE',  ( -0.000000000000000000, -1.000000000000000000, -0.000000000000000000 ) ) ;
#787=CARTESIAN_POINT ( 'NONE',  ( 0.03634916050344778882, 1.602949386431022472, -0.3809527529760087239 ) ) ;
#806=DIRECTION ( 'NONE',  ( 0.000000000000000000, 0.000000000000000000, -1.000000000000000000 ) ) ;
#809=ORIENTED_EDGE ( 'NONE', *, *, #11407, .T. ) ;
#810=DIRECTION ( 'NONE',  ( 0.000000000000000000, 0.000000000000000000, -1.000000000000000000 ) ) ;
#811=CARTESIAN_POINT ( 'NONE',  ( -0.4349147617188414694, 0.7512260236060024354, -0.008611041693271251005 ) ) ;
#822=EDGE_CURVE ( 'NONE', #4210, #2008, #1602, .T. ) ;
#836=CIRCLE ( 'NONE', #13302, 0.4349999999999999423 ) ;
#867=CARTESIAN_POINT ( 'NONE',  ( -0.1444275314249775788, 1.589819979576904130, 0.3809527529760086684 ) ) ;
#884=ADVANCED_FACE ( 'NONE', ( #7508 ), #10805, .T. ) ;
#886=CARTESIAN_POINT ( 'NONE',  ( 0.000000000000000000, 1.109999999999999876, 0.000000000000000000 ) ) ;
#902=CIRCLE ( 'NONE', #7517, 0.1068000000000000754 ) ;
#912=DIRECTION ( 'NONE',  ( -0.000000000000000000, -1.000000000000000000, -0.000000000000000000 ) ) ;
#915=DIRECTION ( 'NONE',  ( 0.000000000000000000, 0.000000000000000000, -1.000000000000000000 ) ) ;
#949=CARTESIAN_POINT ( 'NONE',  ( 0.000000000000000000, 0.000000000000000000, 0.000000000000000000 ) ) ;
#951=CARTESIAN_POINT ( 'NONE',  ( 0.07259084472369427277, 1.600827197418697168, -0.3809527529760087794 ) ) ;
#966=DIRECTION ( 'NONE',  ( -0.000000000000000000, -1.000000000000000000, -0.000000000000000000 ) ) ;
#1021=CARTESIAN_POINT ( 'NONE',  ( 0.2249147617188453907, 1.559103846021540951, 0.3723417112827335784 ) ) ;
#1030=CARTESIAN_POINT ( 'NONE',  ( 0.4349147617188415249, 1.239999999999999991, 0.008611041693268213504 ) ) ;
#1076=CIRCLE ( 'NONE', #96, 0.2499999999999999167 ) ;
#1094=ORIENTED_EDGE ( 'NONE', *, *, #4898, .F. ) ;
#1099=CARTESIAN_POINT ( 'NONE',  ( 0.4313007445438669096, 1.564783867144734497, -0.01487070305975950364 ) ) ;
#1118=ORIENTED_EDGE ( 'NONE', *, *, #3684, .F. ) ;
#1121=ORIENTED_EDGE ( 'NONE', *, *, #4050, .T. ) ;
#1143=DIRECTION ( 'NONE',  ( 0.000000000000000000, 1.000000000000000000, 0.000000000000000000 ) ) ;
#1161=AXIS2_PLACEMENT_3D ( 'NONE', #7424, #6282, #434 ) ;
#1167=DIRECTION ( 'NONE',  ( -0.5000000000000041078, 0.000000000000000000, -0.8660254037844362651 ) ) ;
#1186=DIRECTION ( 'NONE',  ( -0.000000000000000000, -1.000000000000000000, -0.000000000000000000 ) ) ;
#1196=ORIENTED_EDGE ( 'NONE', *, *, #1286, .F. ) ;
#1202=ORIENTED_EDGE ( 'NONE', *, *, #8195, .T. ) ;
#1204=CARTESIAN_POINT ( 'NONE',  ( -0.04538567959942197555, 1.602419810250338861, -0.3809527529760086684 ) ) ;
#1207=CIRCLE ( 'NONE', #9290, 0.4349999999999999978 ) ;
#1210=EDGE_CURVE ( 'NONE', #2101, #6280, #8728, .T. ) ;
#1286=EDGE_CURVE ( 'NONE', #1997, #2748, #14528, .T. ) ;
#1339=CARTESIAN_POINT ( 'NONE',  ( 0.2249147617188453907, 1.559103846021540951, 0.3723417112827335784 ) ) ;
#1367=ORIENTED_EDGE ( 'NONE', *, *, #4089, .T. ) ;
#1386=VERTEX_POINT ( 'NONE', #5515 ) ;
#1401=AXIS2_PLACEMENT_3D ( 'NONE', #4356, #7718, #9097 ) ;
#1423=CARTESIAN_POINT ( 'NONE',  ( 0.1702285915635917413, 1.581112972951822293, 0.3809527529760086684 ) ) ;
#1441=DIRECTION ( 'NONE',  ( 0.000000000000000000, 1.000000000000000000, 0.000000000000000000 ) ) ;
#1452=LINE ( 'NONE', #5140, #13383 ) ;
#1453=EDGE_CURVE ( 'NONE', #6687, #1997, #4112, .T. ) ;
#1477=LINE ( 'NONE', #7751, #13206 ) ;
#1503=CARTESIAN_POINT ( 'NONE',  ( -0.1264631971972069724, 1.593677921218987992, -0.3809527529760086684 ) ) ;
#1521=DIRECTION ( 'NONE',  ( 1.000000000000000000, 0.000000000000000000, 0.000000000000000000 ) ) ;
#1525=PRODUCT_DEFINITION ( 'UNKNOWN', '', #11843, #3110 ) ;
#1580=VECTOR ( 'NONE', #11310, 39.37007874015748143 ) ;
#1600=SHAPE_REPRESENTATION ( 'Hex Bolt', ( #8424 ), #10848 ) ;
#1602=LINE ( 'NONE', #13085, #12748 ) ;
#1616=CYLINDRICAL_SURFACE ( 'NONE', #12564, 0.4349999999999999423 ) ;
#1624=DIRECTION ( 'NONE',  ( 0.000000000000000000, 0.000000000000000000, -1.000000000000000000 ) ) ;
#1669=( LENGTH_UNIT ( ) NAMED_UNIT ( * ) SI_UNIT ( $, .METRE. ) );
#1674=FACE_OUTER_BOUND ( 'NONE', #2096, .T. ) ;
#1683=CARTESIAN_POINT ( 'NONE',  ( 0.2249147617188371751, 1.239999999999999991, -0.3723417112827391295 ) ) ;
#1715=DIRECTION ( 'NONE',  ( 0.000000000000000000, 0.000000000000000000, -1.000000000000000000 ) ) ;
#1735=CARTESIAN_POINT ( 'NONE',  ( 0.4349999999999999978, 1.239999999999999991, 0.000000000000000000 ) ) ;
#1760=CARTESIAN_POINT ( 'NONE',  ( 3.061616997868382402E-17, 1.109999999999999876, 0.2499999999999999167 ) ) ;
#1767=CARTESIAN_POINT ( 'NONE',  ( 0.000000000000000000, 0.000000000000000000, 0.2041999999999996596 ) ) ;
#1768=DIMENSIONAL_EXPONENTS ( 1.000000000000000000, 0.000000000000000000, 0.000000000000000000, 0.000000000000000000, 0.000000000000000000, 0.000000000000000000, 0.000000000000000000 ) ;
#1770=( LENGTH_UNIT ( ) NAMED_UNIT ( * ) SI_UNIT ( $, .METRE. ) );
#1777=AXIS2_PLACEMENT_3D ( 'NONE', #1963, #8941, #14971 ) ;
#1784=VECTOR ( 'NONE', #158, 39.37007874015748143 ) ;
#1806=CARTESIAN_POINT ( 'NONE',  ( -0.3208174396729924216, 1.603403006623433713, -0.2062334004842315271 ) ) ;
#1811=CYLINDRICAL_SURFACE ( 'NONE', #3543, 0.4349999999999999423 ) ;
#1813=CARTESIAN_POINT ( 'NONE',  ( 4.665325695584414469E-17, 1.603403463250997918, 0.3809527529760087239 ) ) ;
#1814=DIRECTION ( 'NONE',  ( 0.8660254037844398178, 0.000000000000000000, 0.4999999999999980016 ) ) ;
#1837=ORIENTED_EDGE ( 'NONE', *, *, #10304, .T. ) ;
#1870=CONICAL_SURFACE ( 'NONE', #7037, 0.2041999999999996596, 0.7853981633974460586 ) ;
#1893=DIRECTION ( 'NONE',  ( 0.000000000000000000, 0.000000000000000000, -1.000000000000000000 ) ) ;
#1894=ORIENTED_EDGE ( 'NONE', *, *, #4747, .F. ) ;
#1927=ORIENTED_EDGE ( 'NONE', *, *, #10850, .F. ) ;
#1936=CIRCLE ( 'NONE', #4635, 0.4850000000000000977 ) ;
#1937=DIRECTION ( 'NONE',  ( 0.000000000000000000, 0.000000000000000000, -1.000000000000000000 ) ) ;
#1938=EDGE_CURVE ( 'NONE', #12744, #6280, #194, .T. ) ;
#1954=DIRECTION ( 'NONE',  ( 0.000000000000000000, 0.000000000000000000, -1.000000000000000000 ) ) ;
#1963=CARTESIAN_POINT ( 'NONE',  ( 0.000000000000000000, 0.000000000000000000, 0.000000000000000000 ) ) ;
#1997=VERTEX_POINT ( 'NONE', #11497 ) ;
#2008=VERTEX_POINT ( 'NONE', #9437 ) ;
#2022=CARTESIAN_POINT ( 'NONE',  ( -0.2099999999999948852, 1.559103846021543616, 0.3809527529760087239 ) ) ;
#2050=ORIENTED_EDGE ( 'NONE', *, *, #3630, .T. ) ;
#2053=DIRECTION ( 'NONE',  ( 0.000000000000000000, 0.000000000000000000, -1.000000000000000000 ) ) ;
#2096=EDGE_LOOP ( 'NONE', ( #8056, #11237, #5998, #11561 ) ) ;
#2100=CARTESIAN_POINT ( 'NONE',  ( -0.01818920831125185600, 1.603403463250997474, 0.3809527529760087239 ) ) ;
#2101=VERTEX_POINT ( 'NONE', #4764 ) ;
#2123=DIRECTION ( 'NONE',  ( -0.000000000000000000, -1.000000000000000000, -0.000000000000000000 ) ) ;
#2144=DIRECTION ( 'NONE',  ( 0.000000000000000000, 1.000000000000000000, 0.000000000000000000 ) ) ;
#2158=ORIENTED_EDGE ( 'NONE', *, *, #9118, .F. ) ;
#2169=FACE_OUTER_BOUND ( 'NONE', #6885, .T. ) ;
#2177=ORIENTED_EDGE ( 'NONE', *, *, #12261, .T. ) ;
#2183=CARTESIAN_POINT ( 'NONE',  ( 0.4274235469976374047, 1.569496918332969226, -0.02158620620081013602 ) ) ;
#2257=CARTESIAN_POINT ( 'NONE',  ( 0.4150689297652778165, 1.581084130983677838, -0.04298503095532220375 ) ) ;
#2269=CARTESIAN_POINT ( 'NONE',  ( 0.2447605936724075171, 1.581084130983678060, 0.3379677220206893096 ) ) ;
#2321=DIRECTION ( 'NONE',  ( -0.000000000000000000, -1.000000000000000000, -0.000000000000000000 ) ) ;
#2409=CARTESIAN_POINT ( 'NONE',  ( 0.2099999999999999922, 1.559103846021543172, -0.3809527529760087239 ) ) ;
#2430=DIRECTION ( 'NONE',  ( -0.8660254037844328234, 0.000000000000000000, 0.5000000000000101030 ) ) ;
#2432=AXIS2_PLACEMENT_3D ( 'NONE', #5872, #7378, #3571 ) ;
#2438=CARTESIAN_POINT ( 'NONE',  ( 0.4019514777495877822, 1.589927591219149727, 0.06570512431233779815 ) ) ;
#2511=ORIENTED_EDGE ( 'NONE', *, *, #11180, .T. ) ;
#2548=ORIENTED_EDGE ( 'NONE', *, *, #4519, .T. ) ;
#2565=ORIENTED_EDGE ( 'NONE', *, *, #10757, .F. ) ;
#2611=EDGE_CURVE ( 'NONE', #2748, #3130, #4056, .T. ) ;
#2629=CARTESIAN_POINT ( 'NONE',  ( -0.2249147617188618498, 1.559103846021574258, 0.3723417112826993836 ) ) ;
#2639=VERTEX_POINT ( 'NONE', #12219 ) ;
#2740=CARTESIAN_POINT ( 'NONE',  ( 0.000000000000000000, 0.000000000000000000, 0.000000000000000000 ) ) ;
#2748=VERTEX_POINT ( 'NONE', #4786 ) ;
#2776=ADVANCED_FACE ( 'NONE', ( #13023 ), #8322, .F. ) ;
#2785=LINE ( 'NONE', #1767, #5454 ) ;
#2799=ORIENTED_EDGE ( 'NONE', *, *, #5375, .T. ) ;
#2809=SHAPE_DEFINITION_REPRESENTATION ( #7272, #1600 ) ;
#2829=DIRECTION ( 'NONE',  ( 0.000000000000000000, -0.000000000000000000, 1.000000000000000000 ) ) ;
#2839=VERTEX_POINT ( 'NONE', #2409 ) ;
#2898=CARTESIAN_POINT ( 'NONE',  ( -0.3752176239131143065, 1.599166939805956034, -0.1120095174392321397 ) ) ;
#2919=VERTEX_POINT ( 'NONE', #7448 ) ;
#2955=DIRECTION ( 'NONE',  ( -0.000000000000000000, -1.000000000000000000, -0.000000000000000000 ) ) ;
#3011=ADVANCED_FACE ( 'NONE', ( #9975 ), #1616, .T. ) ;
#3051=FACE_BOUND ( 'NONE', #12082, .T. ) ;
#3097=DIRECTION ( 'NONE',  ( -0.000000000000000000, -1.000000000000000000, -0.000000000000000000 ) ) ;
#3110=PRODUCT_DEFINITION_CONTEXT ( 'detailed design', #3426, 'design' ) ;
#3121=CARTESIAN_POINT ( 'NONE',  ( 0.000000000000000000, 1.559103846021539619, 0.000000000000000000 ) ) ;
#3130=VERTEX_POINT ( 'NONE', #6531 ) ;
#3142=CARTESIAN_POINT ( 'NONE',  ( 0.2249147617188371751, 1.239999999999999991, -0.3723417112827391295 ) ) ;
#3157=AXIS2_PLACEMENT_3D ( 'NONE', #2740, #3746, #3816 ) ;
#3164=CARTESIAN_POINT ( 'NONE',  ( 0.4349147617188415249, 1.559103846021539619, 0.008611041693268213504 ) ) ;
#3183=ORIENTED_EDGE ( 'NONE', *, *, #5627, .T. ) ;
#3193=CARTESIAN_POINT ( 'NONE',  ( -0.1702344636782962828, 1.581111061277888252, 0.3809527529760087239 ) ) ;
#3208=CARTESIAN_POINT ( 'NONE',  ( 0.000000000000000000, 1.559103846021539619, 0.000000000000000000 ) ) ;
#3210=DIRECTION ( 'NONE',  ( 0.000000000000000000, 0.000000000000000000, 1.000000000000000000 ) ) ;
#3230=DIRECTION ( 'NONE',  ( -0.000000000000000000, -1.000000000000000000, -0.000000000000000000 ) ) ;
#3257=CARTESIAN_POINT ( 'NONE',  ( -0.4349147617188415249, 1.239999999999999991, 0.008611041693274120237 ) ) ;
#3310=ADVANCED_FACE ( 'NONE', ( #2169, #9300 ), #10435, .T. ) ;
#3347=CARTESIAN_POINT ( 'NONE',  ( 0.3389861398596112907, 1.603403919227001095, 0.1747642886535209217 ) ) ;
#3412=CARTESIAN_POINT ( 'NONE',  ( -0.2665675396067773706, 1.593633255602467935, -0.3001969837044509148 ) ) ;
#3419=EDGE_CURVE ( 'NONE', #12744, #14900, #3977, .T. ) ;
#3424=CARTESIAN_POINT ( 'NONE',  ( 0.2577064312470200291, 1.589827634136293355, 0.3155448735949257788 ) ) ;
#3426=APPLICATION_CONTEXT ( 'automotive_design' ) ;
#3437=DIRECTION ( 'NONE',  ( -1.000000000000000000, 0.000000000000000000, 0.000000000000000000 ) ) ;
#3464=CIRCLE ( 'NONE', #4446, 0.2041999999999996596 ) ;
#3470=VERTEX_POINT ( 'NONE', #1813 ) ;
#3498=CARTESIAN_POINT ( 'NONE',  ( 0.2936128187763883957, 1.600826314462300282, 0.2533531860778008293 ) ) ;
#3509=CARTESIAN_POINT ( 'NONE',  ( -0.1444440947987238599, 1.589814529920261732, -0.3809527529760087239 ) ) ;
#3533=LINE ( 'NONE', #5840, #9420 ) ;
#3543=AXIS2_PLACEMENT_3D ( 'NONE', #13363, #11079, #9725 ) ;
#3563=UNCERTAINTY_MEASURE_WITH_UNIT (LENGTH_MEASURE( 1.000000000000000082E-05 ), #4167, 'distance_accuracy_value', 'NONE');
#3567=CARTESIAN_POINT ( 'NONE',  ( 0.3390120837646757312, 1.603403006623434379, -0.1747193524918033425 ) ) ;
#3571=DIRECTION ( 'NONE',  ( 1.000000000000000000, 0.000000000000000000, 0.000000000000000000 ) ) ;
#3594=CARTESIAN_POINT ( 'NONE',  ( 0.2249147617188449189, 0.7512260236060024354, 0.3723417112827343556 ) ) ;
#3605=EDGE_LOOP ( 'NONE', ( #14641, #8107, #6723, #13180 ) ) ;
#3611=CARTESIAN_POINT ( 'NONE',  ( 0.2099999999999999922, 1.559103846021539619, 0.3809527529760087239 ) ) ;
#3630=EDGE_CURVE ( 'NONE', #6280, #3743, #5585, .T. ) ;
#3633=ADVANCED_FACE ( 'NONE', ( #9177 ), #15061, .T. ) ;
#3648=CARTESIAN_POINT ( 'NONE',  ( 0.3117353328467041274, 1.602948811930422712, -0.2219640709471300821 ) ) ;
#3665=CARTESIAN_POINT ( 'NONE',  ( 0.2405080627748377164, 1.577645543303439313, 0.3453333215960370794 ) ) ;
#3667=EDGE_CURVE ( 'NONE', #710, #13032, #902, .T. ) ;
#3684=EDGE_CURVE ( 'NONE', #13770, #13032, #9490, .T. ) ;
#3689=ORIENTED_EDGE ( 'NONE', *, *, #9786, .T. ) ;
#3705=EDGE_CURVE ( 'NONE', #8521, #9230, #9412, .T. ) ;
#3736=ORIENTED_EDGE ( 'NONE', *, *, #9164, .F. ) ;
#3743=VERTEX_POINT ( 'NONE', #12983 ) ;
#3746=DIRECTION ( 'NONE',  ( -0.000000000000000000, -1.000000000000000000, -0.000000000000000000 ) ) ;
#3777=CARTESIAN_POINT ( 'NONE',  ( -0.3480879174158268419, 1.602949672542212989, 0.1589995474869664860 ) ) ;
#3791=FACE_OUTER_BOUND ( 'NONE', #13343, .T. ) ;
#3816=DIRECTION ( 'NONE',  ( 0.000000000000000000, 0.000000000000000000, -1.000000000000000000 ) ) ;
#3834=ORIENTED_EDGE ( 'NONE', *, *, #14195, .F. ) ;
#3847=VECTOR ( 'NONE', #11058, 39.37007874015748143 ) ;
#3848=CARTESIAN_POINT ( 'NONE',  ( 0.000000000000000000, 0.000000000000000000, 0.000000000000000000 ) ) ;
#3854=ORIENTED_EDGE ( 'NONE', *, *, #4089, .F. ) ;
#3857=CARTESIAN_POINT ( 'NONE',  ( -0.4274235469976391255, 1.569496918332966784, 0.02158620620080434552 ) ) ;
#3861=VECTOR ( 'NONE', #8274, 39.37007874015747433 ) ;
#3872=CARTESIAN_POINT ( 'NONE',  ( 0.000000000000000000, 1.109999999999999876, 0.000000000000000000 ) ) ;
#3884=AXIS2_PLACEMENT_3D ( 'NONE', #5337, #7481, #6264 ) ;
#3924=DIRECTION ( 'NONE',  ( -0.000000000000000000, -1.000000000000000000, -0.000000000000000000 ) ) ;
#3948=DIRECTION ( 'NONE',  ( -0.000000000000000000, -1.000000000000000000, -0.000000000000000000 ) ) ;
#3955=CARTESIAN_POINT ( 'NONE',  ( 0.04538567959942203800, 1.602419810250338861, 0.3809527529760087239 ) ) ;
#3972=ORIENTED_EDGE ( 'NONE', *, *, #4898, .T. ) ;
#3977=LINE ( 'NONE', #9867, #15036 ) ;
#3992=CARTESIAN_POINT ( 'NONE',  ( -0.2667400994511678891, 1.593697031032158318, 0.2998981012866184237 ) ) ;
#4031=DIRECTION ( 'NONE',  ( -0.4999999999999918954, 0.000000000000000000, 0.8660254037844431485 ) ) ;
#4050=EDGE_CURVE ( 'NONE', #2101, #5835, #4914, .T. ) ;
#4055=PLANE ( 'NONE',  #14622 ) ;
#4056=CIRCLE ( 'NONE', #12848, 0.2499999999999999167 ) ;
#4069=CARTESIAN_POINT ( 'NONE',  ( -0.2285544654201572545, 1.564824237736550439, 0.3660375595475592325 ) ) ;
#4089=EDGE_CURVE ( 'NONE', #14900, #13770, #14298, .T. ) ;
#4103=CARTESIAN_POINT ( 'NONE',  ( 0.03632416821535690982, 1.602793162442987418, 0.3809527529760087794 ) ) ;
#4104=LINE ( 'NONE', #6403, #3847 ) ;
#4112=CIRCLE ( 'NONE', #15104, 0.2041999999999996596 ) ;
#4114=B_SPLINE_CURVE_WITH_KNOTS ( 'NONE', 3,
 ( #6782, #10295, #11358, #7634, #13357, #11441, #571, #2898, #5267, #4412, #14885, #1806, #12296, #7565, #6421, #3412, #4481, #14957, #9939, #12226, #9150, #14594 ),
 .UNSPECIFIED., .F., .F.,
 ( 4, 2, 2, 2, 2, 2, 2, 2, 2, 2, 4 ),
 ( 2.884201068394857235E-07, 0.0006930185370347780819, 0.001385748653962716676, 0.002771208887818601887, 0.004156669121674489049, 0.005542129355530375778, 0.006927589589386263375, 0.008313049823242149236, 0.009698510057098036832, 0.01039124017402597716, 0.01108397029095391749 ),
 .UNSPECIFIED. ) ;
#4167=( CONVERSION_BASED_UNIT ( 'INCH', #5228 ) LENGTH_UNIT ( ) NAMED_UNIT ( #1768 ) );
#4182=VERTEX_POINT ( 'NONE', #7497 ) ;
#4188=CARTESIAN_POINT ( 'NONE',  ( -0.09067304051454433411, 1.599165379501958695, 0.3809527529760087239 ) ) ;
#4194=ADVANCED_FACE ( 'NONE', ( #3051, #12080 ), #12230, .T. ) ;
#4210=VERTEX_POINT ( 'NONE', #10027 ) ;
#4225=EDGE_LOOP ( 'NONE', ( #8061, #4656 ) ) ;
#4257=ORIENTED_EDGE ( 'NONE', *, *, #3667, .F. ) ;
#4259=CARTESIAN_POINT ( 'NONE',  ( 0.2846118995245459082, 1.599166939805951593, -0.2689432355368134853 ) ) ;
#4262=CARTESIAN_POINT ( 'NONE',  ( -0.1787546228633429546, 1.577672892097735646, 0.3809527529760086129 ) ) ;
#4264=CIRCLE ( 'NONE', #12796, 0.4349999999999999423 ) ;
#4281=ADVANCED_FACE ( 'NONE', ( #13216 ), #12401, .T. ) ;
#4290=EDGE_CURVE ( 'NONE', #6222, #4182, #6794, .T. ) ;
#4311=EDGE_CURVE ( 'NONE', #8521, #7375, #8017, .T. ) ;
#4356=CARTESIAN_POINT ( 'NONE',  ( 0.000000000000000000, 1.239999999999999991, 0.000000000000000000 ) ) ;
#4375=CYLINDRICAL_SURFACE ( 'NONE', #558, 0.4349999999999999423 ) ;
#4412=CARTESIAN_POINT ( 'NONE',  ( -0.3480941905909599177, 1.602948811930424711, -0.1589886820289102831 ) ) ;
#4446=AXIS2_PLACEMENT_3D ( 'NONE', #5530, #912, #9122 ) ;
#4467=CARTESIAN_POINT ( 'NONE',  ( 0.000000000000000000, 1.239999999999999991, 0.000000000000000000 ) ) ;
#4481=CARTESIAN_POINT ( 'NONE',  ( -0.2577064312470127572, 1.589827634136290468, -0.3155448735949362149 ) ) ;
#4486=CARTESIAN_POINT ( 'NONE',  ( 0.1266950372298308314, 1.593635284016129416, -0.3809527529760087239 ) ) ;
#4502=CARTESIAN_POINT ( 'NONE',  ( 3.061616997868382402E-17, 0.000000000000000000, 0.2499999999999999167 ) ) ;
#4519=EDGE_CURVE ( 'NONE', #5884, #14900, #385, .T. ) ;
#4634=DIRECTION ( 'NONE',  ( 0.8660254037844362651, 0.000000000000000000, -0.5000000000000041078 ) ) ;
#4635=AXIS2_PLACEMENT_3D ( 'NONE', #8212, #5837, #12542 ) ;
#4641=CARTESIAN_POINT ( 'NONE',  ( 0.4349147617188408588, 1.559103846021540951, -0.008611041693278118775 ) ) ;
#4650=FACE_OUTER_BOUND ( 'NONE', #8558, .T. ) ;
#4654=CARTESIAN_POINT ( 'NONE',  ( 0.2665675396067855862, 1.593633255602470156, 0.3001969837044382028 ) ) ;
#4656=ORIENTED_EDGE ( 'NONE', *, *, #383, .F. ) ;
#4660=DIRECTION ( 'NONE',  ( 0.000000000000000000, 0.000000000000000000, -1.000000000000000000 ) ) ;
#4677=ADVANCED_FACE ( 'NONE', ( #5113 ), #7405, .T. ) ;
#4684=EDGE_CURVE ( 'NONE', #5884, #13214, #4104, .T. ) ;
#4691=ADVANCED_FACE ( 'NONE', ( #8776 ), #5249, .T. ) ;
#4720=FACE_OUTER_BOUND ( 'NONE', #13211, .T. ) ;
#4728=CARTESIAN_POINT ( 'NONE',  ( 0.3930894239865358464, 1.593697031032150102, 0.08105465168935101217 ) ) ;
#4733=CARTESIAN_POINT ( 'NONE',  ( 0.000000000000000000, 1.239999999999999991, 0.000000000000000000 ) ) ;
#4739=FACE_OUTER_BOUND ( 'NONE', #13425, .T. ) ;
#4747=EDGE_CURVE ( 'NONE', #1386, #14655, #14808, .T. ) ;
#4752=ADVANCED_FACE ( 'NONE', ( #11445 ), #10299, .T. ) ;
#4764=CARTESIAN_POINT ( 'NONE',  ( 0.4349147617188414694, 1.239999999999999991, -0.008611041693277159473 ) ) ;
#4786=CARTESIAN_POINT ( 'NONE',  ( 0.000000000000000000, 0.04580000000000046534, -0.2499999999999999167 ) ) ;
#4795=DIRECTION ( 'NONE',  ( -0.000000000000000000, 1.000000000000000000, -0.000000000000000000 ) ) ;
#4819=CARTESIAN_POINT ( 'NONE',  ( -0.03632416821535707635, 1.602793162442987418, -0.3809527529760087794 ) ) ;
#4823=AXIS2_PLACEMENT_3D ( 'NONE', #6257, #9771, #1715 ) ;
#4834=VERTEX_POINT ( 'NONE', #1021 ) ;
#4875=CARTESIAN_POINT ( 'NONE',  ( 0.3753013551531362291, 1.599152118624413976, -0.1118644906773359898 ) ) ;
#4898=EDGE_CURVE ( 'NONE', #12744, #2839, #94, .T. ) ;
#4901=CARTESIAN_POINT ( 'NONE',  ( -0.1949587543783453114, 1.569534359386388411, -0.3809527529760086684 ) ) ;
#4914=LINE ( 'NONE', #14155, #14357 ) ;
#4916=( NAMED_UNIT ( * ) SI_UNIT ( $, .STERADIAN. ) SOLID_ANGLE_UNIT ( ) );
#4927=ORIENTED_EDGE ( 'NONE', *, *, #4519, .F. ) ;
#4933=CARTESIAN_POINT ( 'NONE',  ( -0.3390120837646902197, 1.603403006623433491, 0.1747193524917784735 ) ) ;
#5006=CARTESIAN_POINT ( 'NONE',  ( -0.3662167046613059029, 1.600826314462298061, 0.1275995668981904640 ) ) ;
#5030=EDGE_CURVE ( 'NONE', #2008, #2639, #13466, .T. ) ;
#5038=LINE ( 'NONE', #9697, #12624 ) ;
#5062=CARTESIAN_POINT ( 'NONE',  ( 0.000000000000000000, 0.000000000000000000, 0.000000000000000000 ) ) ;
#5113=FACE_OUTER_BOUND ( 'NONE', #7701, .T. ) ;
#5134=AXIS2_PLACEMENT_3D ( 'NONE', #6082, #9303, #10748 ) ;
#5140=CARTESIAN_POINT ( 'NONE',  ( 0.2099999999999999922, 0.7512260236060024354, 0.3809527529760087239 ) ) ;
#5152=CARTESIAN_POINT ( 'NONE',  ( -0.3753013551531455549, 1.599152118624412644, 0.1118644906773185593 ) ) ;
#5177=CARTESIAN_POINT ( 'NONE',  ( 0.1786439721334352748, 1.577722767886655886, 0.3809527529760086684 ) ) ;
#5199=( CONVERSION_BASED_UNIT ( 'INCH', #507 ) LENGTH_UNIT ( ) NAMED_UNIT ( #8539 ) );
#5213=DIRECTION ( 'NONE',  ( -0.000000000000000000, -1.000000000000000000, -0.000000000000000000 ) ) ;
#5218=EDGE_CURVE ( 'NONE', #1997, #6687, #3464, .T. ) ;
#5228=LENGTH_MEASURE_WITH_UNIT ( LENGTH_MEASURE( 0.02539999999999999897 ), #1770 );
#5249=CYLINDRICAL_SURFACE ( 'NONE', #5549, 0.4349999999999999423 ) ;
#5267=CARTESIAN_POINT ( 'NONE',  ( -0.3662050505264201616, 1.600827805288695949, -0.1276197524519294968 ) ) ;
#5280=EDGE_CURVE ( 'NONE', #13770, #13214, #7391, .T. ) ;
#5289=CARTESIAN_POINT ( 'NONE',  ( -0.2249147617188618498, 1.559103846021574258, 0.3723417112826993836 ) ) ;
#5291=CARTESIAN_POINT ( 'NONE',  ( 5.939536975864662229E-17, 1.239999999999999991, 0.4849999999999999312 ) ) ;
#5329=CARTESIAN_POINT ( 'NONE',  ( 0.2324505233676561755, 1.569549437900746414, -0.3592893892332560402 ) ) ;
#5332=AXIS2_PLACEMENT_3D ( 'NONE', #9587, #6059, #10724 ) ;
#5337=CARTESIAN_POINT ( 'NONE',  ( 0.000000000000000000, 0.04580000000000046534, 0.000000000000000000 ) ) ;
#5360=AXIS2_PLACEMENT_3D ( 'NONE', #15039, #786, #1954 ) ;
#5364=DIRECTION ( 'NONE',  ( 2.930988785010413267E-14, 0.000000000000000000, -1.000000000000000000 ) ) ;
#5375=EDGE_CURVE ( 'NONE', #3743, #2839, #6626, .T. ) ;
#5389=( NAMED_UNIT ( * ) SI_UNIT ( $, .STERADIAN. ) SOLID_ANGLE_UNIT ( ) );
#5442=DIRECTION ( 'NONE',  ( 0.000000000000000000, 0.000000000000000000, -1.000000000000000000 ) ) ;
#5448=CIRCLE ( 'NONE', #13976, 0.3440000000000000280 ) ;
#5454=VECTOR ( 'NONE', #6383, 39.37007874015748854 ) ;
#5480=DIRECTION ( 'NONE',  ( -0.4999999999999979461, 0.000000000000000000, 0.8660254037844397068 ) ) ;
#5483=CARTESIAN_POINT ( 'NONE',  ( -0.03634916050344735167, 1.602949386431022694, 0.3809527529760086684 ) ) ;
#5493=ADVANCED_FACE ( 'NONE', ( #4650 ), #7254, .F. ) ;
#5500=ORIENTED_EDGE ( 'NONE', *, *, #10850, .T. ) ;
#5515=CARTESIAN_POINT ( 'NONE',  ( -0.2100000000000001865, 1.239999999999999991, 0.3809527529760087239 ) ) ;
#5530=CARTESIAN_POINT ( 'NONE',  ( 0.000000000000000000, 0.000000000000000000, 0.000000000000000000 ) ) ;
#5546=VERTEX_POINT ( 'NONE', #3164 ) ;
#5549=AXIS2_PLACEMENT_3D ( 'NONE', #13421, #2955, #7617 ) ;
#5552=ORIENTED_EDGE ( 'NONE', *, *, #7455, .T. ) ;
#5560=DIRECTION ( 'NONE',  ( 0.000000000000000000, 0.000000000000000000, -1.000000000000000000 ) ) ;
#5562=CARTESIAN_POINT ( 'NONE',  ( 0.1950126918253253516, 1.569501570604563856, -0.3809527529760087239 ) ) ;
#5585=LINE ( 'NONE', #6656, #1580 ) ;
#5616=MANIFOLD_SOLID_BREP ( 'Cut-Revolve1', #10599 ) ;
#5627=EDGE_CURVE ( 'NONE', #6554, #12746, #1477, .T. ) ;
#5652=FACE_OUTER_BOUND ( 'NONE', #11885, .T. ) ;
#5679=DIRECTION ( 'NONE',  ( 0.000000000000000000, -0.000000000000000000, 1.000000000000000000 ) ) ;
#5715=CARTESIAN_POINT ( 'NONE',  ( -0.1950126918253222708, 1.569501570604565632, 0.3809527529760086129 ) ) ;
#5720=CARTESIAN_POINT ( 'NONE',  ( 0.2249147617188371751, 0.7512260236060024354, -0.3723417112827391295 ) ) ;
#5752=PLANE ( 'NONE',  #12196 ) ;
#5819=B_SPLINE_CURVE_WITH_KNOTS ( 'NONE', 3,
 ( #12742, #11836, #9478, #35, #7034, #2438, #4728, #6029, #13888, #10463, #3347, #9402, #14125, #3498, #6952, #4654, #3424, #2269, #3665, #12821, #10541, #1339 ),
 .UNSPECIFIED., .F., .F.,
 ( 4, 2, 2, 2, 2, 2, 2, 2, 2, 2, 4 ),
 ( 2.884201054326571187E-07, 0.0006930185370334598005, 0.001385748653961486974, 0.002771208887817543706, 0.004156669121673600004, 0.005542129355529658470, 0.006927589589385716069, 0.008313049823241772801, 0.009698510057097830400, 0.01039124017402585226, 0.01108397029095387412 ),
 .UNSPECIFIED. ) ;
#5835=VERTEX_POINT ( 'NONE', #10832 ) ;
#5837=DIRECTION ( 'NONE',  ( -0.000000000000000000, -1.000000000000000000, -0.000000000000000000 ) ) ;
#5839=ADVANCED_BREP_SHAPE_REPRESENTATION ( '', ( #5616, #8424 ), #10848 ) ;
#5840=CARTESIAN_POINT ( 'NONE',  ( 5.939536975864663462E-17, 0.000000000000000000, 0.4850000000000000422 ) ) ;
#5844=ORIENTED_EDGE ( 'NONE', *, *, #5627, .F. ) ;
#5870=CARTESIAN_POINT ( 'NONE',  ( 0.3932619838308991644, 1.593633255602470156, -0.08075576927157292195 ) ) ;
#5872=CARTESIAN_POINT ( 'NONE',  ( -0.2099999999999999922, 0.7512260236060024354, -0.3809527529760087239 ) ) ;
#5884=VERTEX_POINT ( 'NONE', #11128 ) ;
#5896=CARTESIAN_POINT ( 'NONE',  ( 0.000000000000000000, 1.603403463250997918, -0.3809527529760087239 ) ) ;
#5902=ORIENTED_EDGE ( 'NONE', *, *, #9222, .F. ) ;
#5923=DIRECTION ( 'NONE',  ( 0.000000000000000000, 1.000000000000000000, 0.000000000000000000 ) ) ;
#5977=ORIENTED_EDGE ( 'NONE', *, *, #10876, .T. ) ;
#5993=ORIENTED_EDGE ( 'NONE', *, *, #8516, .F. ) ;
#5998=ORIENTED_EDGE ( 'NONE', *, *, #4684, .F. ) ;
#6011=ORIENTED_EDGE ( 'NONE', *, *, #12876, .F. ) ;
#6029=CARTESIAN_POINT ( 'NONE',  ( 0.3752176239131347346, 1.599166939805951593, 0.1120095174391954607 ) ) ;
#6059=DIRECTION ( 'NONE',  ( -0.000000000000000000, -1.000000000000000000, -0.000000000000000000 ) ) ;
#6082=CARTESIAN_POINT ( 'NONE',  ( 0.000000000000000000, 1.503199999999999870, 0.000000000000000000 ) ) ;
#6113=VERTEX_POINT ( 'NONE', #12836 ) ;
#6117=DIRECTION ( 'NONE',  ( -0.000000000000000000, -1.000000000000000000, -0.000000000000000000 ) ) ;
#6120=ORIENTED_EDGE ( 'NONE', *, *, #3705, .F. ) ;
#6130=DIRECTION ( 'NONE',  ( -5.329070518200750763E-14, 0.000000000000000000, -1.000000000000000000 ) ) ;
#6134=ORIENTED_EDGE ( 'NONE', *, *, #3705, .T. ) ;
#6151=CARTESIAN_POINT ( 'NONE',  ( -0.2936244729112616469, 1.600827805288695949, 0.2533330005240802540 ) ) ;
#6171=LINE ( 'NONE', #10831, #8773 ) ;
#6182=CARTESIAN_POINT ( 'NONE',  ( 0.07252880680210851971, 1.600831684639946850, 0.3809527529760087239 ) ) ;
#6222=VERTEX_POINT ( 'NONE', #1760 ) ;
#6257=CARTESIAN_POINT ( 'NONE',  ( 0.2499999999999999722, 0.000000000000000000, 0.000000000000000000 ) ) ;
#6264=DIRECTION ( 'NONE',  ( 0.000000000000000000, 0.000000000000000000, -1.000000000000000000 ) ) ;
#6280=VERTEX_POINT ( 'NONE', #3142 ) ;
#6282=DIRECTION ( 'NONE',  ( 0.000000000000000000, 1.000000000000000000, 0.000000000000000000 ) ) ;
#6330=ORIENTED_EDGE ( 'NONE', *, *, #822, .F. ) ;
#6353=ORIENTED_EDGE ( 'NONE', *, *, #4290, .T. ) ;
#6383=DIRECTION ( 'NONE',  ( 0.000000000000000000, 0.7071067811865490160, 0.7071067811865459074 ) ) ;
#6387=EDGE_CURVE ( 'NONE', #7567, #14655, #4264, .T. ) ;
#6391=PLANE ( 'NONE',  #13113 ) ;
#6403=CARTESIAN_POINT ( 'NONE',  ( -0.2249147617188423653, 0.7512260236060024354, -0.3723417112827359654 ) ) ;
#6421=CARTESIAN_POINT ( 'NONE',  ( -0.2845281682845372528, 1.599152118624411756, -0.2690882622986915385 ) ) ;
#6429=DIRECTION ( 'NONE',  ( -1.000000000000000000, 0.000000000000000000, -0.000000000000000000 ) ) ;
#6445=ORIENTED_EDGE ( 'NONE', *, *, #519, .F. ) ;
#6486=CIRCLE ( 'NONE', #6744, 0.4349999999999999423 ) ;
#6501=FACE_OUTER_BOUND ( 'NONE', #10469, .T. ) ;
#6513=CARTESIAN_POINT ( 'NONE',  ( 0.000000000000000000, 0.000000000000000000, 0.000000000000000000 ) ) ;
#6531=CARTESIAN_POINT ( 'NONE',  ( 3.061616997868382402E-17, 0.04580000000000046534, 0.2499999999999999167 ) ) ;
#6533=ADVANCED_FACE ( 'NONE', ( #14842 ), #4375, .T. ) ;
#6536=ORIENTED_EDGE ( 'NONE', *, *, #6754, .T. ) ;
#6551=ORIENTED_EDGE ( 'NONE', *, *, #11180, .F. ) ;
#6554=VERTEX_POINT ( 'NONE', #11633 ) ;
#6561=CARTESIAN_POINT ( 'NONE',  ( 0.2099999999999999922, 1.559103846021543172, -0.3809527529760087239 ) ) ;
#6626=CIRCLE ( 'NONE', #14190, 0.4349999999999999423 ) ;
#6640=CARTESIAN_POINT ( 'NONE',  ( 0.000000000000000000, 1.559103846021539619, 0.000000000000000000 ) ) ;
#6650=ORIENTED_EDGE ( 'NONE', *, *, #10501, .T. ) ;
#6656=CARTESIAN_POINT ( 'NONE',  ( 0.2249147617188371751, 0.7512260236060024354, -0.3723417112827391295 ) ) ;
#6684=ORIENTED_EDGE ( 'NONE', *, *, #4290, .F. ) ;
#6687=VERTEX_POINT ( 'NONE', #14508 ) ;
#6703=DIRECTION ( 'NONE',  ( -0.000000000000000000, -1.000000000000000000, -0.000000000000000000 ) ) ;
#6705=CARTESIAN_POINT ( 'NONE',  ( 0.01818920831125209192, 1.603403463250998584, -0.3809527529760088904 ) ) ;
#6711=DIRECTION ( 'NONE',  ( 0.000000000000000000, 1.000000000000000000, 0.000000000000000000 ) ) ;
#6723=ORIENTED_EDGE ( 'NONE', *, *, #4311, .F. ) ;
#6734=AXIS2_PLACEMENT_3D ( 'NONE', #11619, #12281, #4031 ) ;
#6744=AXIS2_PLACEMENT_3D ( 'NONE', #11739, #5923, #10581 ) ;
#6754=EDGE_CURVE ( 'NONE', #5546, #5835, #12550, .T. ) ;
#6772=AXIS2_PLACEMENT_3D ( 'NONE', #949, #6703, #5560 ) ;
#6782=CARTESIAN_POINT ( 'NONE',  ( -0.4349147617188193760, 1.559103846021574480, -0.008611041693309614414 ) ) ;
#6794=CIRCLE ( 'NONE', #14118, 0.2499999999999999167 ) ;
#6832=ORIENTED_EDGE ( 'NONE', *, *, #8401, .F. ) ;
#6833=ORIENTED_EDGE ( 'NONE', *, *, #8664, .F. ) ;
#6842=ADVANCED_FACE ( 'NONE', ( #5652 ), #14674, .T. ) ;
#6854=DIRECTION ( 'NONE',  ( 0.000000000000000000, -1.000000000000000000, -0.000000000000000000 ) ) ;
#6884=LINE ( 'NONE', #4502, #12855 ) ;
#6885=EDGE_LOOP ( 'NONE', ( #11993, #13468 ) ) ;
#6893=( GEOMETRIC_REPRESENTATION_CONTEXT ( 3 ) GLOBAL_UNCERTAINTY_ASSIGNED_CONTEXT ( ( #3563 ) ) GLOBAL_UNIT_ASSIGNED_CONTEXT ( ( #4167, #7674, #5389 ) ) REPRESENTATION_CONTEXT ( 'NONE', 'WORKASPACE' ) );
#6907=EDGE_CURVE ( 'NONE', #5546, #4834, #5819, .T. ) ;
#6939=CARTESIAN_POINT ( 'NONE',  ( 0.2936244729112413299, 1.600827805288693062, -0.2533330005241143934 ) ) ;
#6952=CARTESIAN_POINT ( 'NONE',  ( 0.2845281682845477444, 1.599152118624413976, 0.2690882622986748296 ) ) ;
#6982=ORIENTED_EDGE ( 'NONE', *, *, #9050, .F. ) ;
#6985=AXIS2_PLACEMENT_3D ( 'NONE', #11262, #3230, #12706 ) ;
#7034=CARTESIAN_POINT ( 'NONE',  ( 0.4150198198414020156, 1.581125151349147773, 0.04307009183862406387 ) ) ;
#7037=AXIS2_PLACEMENT_3D ( 'NONE', #14416, #14334, #9904 ) ;
#7043=ORIENTED_EDGE ( 'NONE', *, *, #4747, .T. ) ;
#7061=DIRECTION ( 'NONE',  ( -0.000000000000000000, 1.000000000000000000, -0.000000000000000000 ) ) ;
#7067=APPLICATION_CONTEXT ( 'automotive_design' ) ;
#7102=ORIENTED_EDGE ( 'NONE', *, *, #9050, .T. ) ;
#7114=DIRECTION ( 'NONE',  ( -0.000000000000000000, -1.000000000000000000, -0.000000000000000000 ) ) ;
#7158=ORIENTED_EDGE ( 'NONE', *, *, #14769, .F. ) ;
#7231=CARTESIAN_POINT ( 'NONE',  ( -0.2099999999999948852, 1.559103846021543616, 0.3809527529760087239 ) ) ;
#7232=ORIENTED_EDGE ( 'NONE', *, *, #5218, .T. ) ;
#7234=FACE_OUTER_BOUND ( 'NONE', #7499, .T. ) ;
#7254=PLANE ( 'NONE',  #9799 ) ;
#7272=PRODUCT_DEFINITION_SHAPE ( 'NONE', 'NONE',  #1525 ) ;
#7278=CARTESIAN_POINT ( 'NONE',  ( 0.000000000000000000, 1.559103846021539619, 0.000000000000000000 ) ) ;
#7306=CARTESIAN_POINT ( 'NONE',  ( -0.3117353328467220019, 1.602948811930424267, 0.2219640709470993845 ) ) ;
#7324=DIRECTION ( 'NONE',  ( -0.000000000000000000, -1.000000000000000000, -0.000000000000000000 ) ) ;
#7330=EDGE_CURVE ( 'NONE', #7375, #392, #12947, .T. ) ;
#7336=ORIENTED_EDGE ( 'NONE', *, *, #2611, .T. ) ;
#7342=CARTESIAN_POINT ( 'NONE',  ( -0.2028461515626820144, 1.564725569476186573, -0.3809527529760086684 ) ) ;
#7358=DIRECTION ( 'NONE',  ( 0.000000000000000000, 0.000000000000000000, 1.000000000000000000 ) ) ;
#7373=STYLED_ITEM('',(#15199),#5616);
#7375=VERTEX_POINT ( 'NONE', #10662 ) ;
#7378=DIRECTION ( 'NONE',  ( -0.000000000000000000, 0.000000000000000000, 1.000000000000000000 ) ) ;
#7391=CIRCLE ( 'NONE', #757, 0.4349999999999999423 ) ;
#7404=CARTESIAN_POINT ( 'NONE',  ( 0.009170202274340883905, 1.603403463250997918, 0.3809527529760087239 ) ) ;
#7405=PLANE ( 'NONE',  #4823 ) ;
#7413=DIRECTION ( 'NONE',  ( 0.000000000000000000, 1.000000000000000000, 0.000000000000000000 ) ) ;
#7424=CARTESIAN_POINT ( 'NONE',  ( 0.000000000000000000, 0.000000000000000000, 0.000000000000000000 ) ) ;
#7439=CARTESIAN_POINT ( 'NONE',  ( -0.2448097035963034407, 1.581125151349165314, 0.3378826611373411115 ) ) ;
#7448=CARTESIAN_POINT ( 'NONE',  ( 4.769999282678940657E-17, 1.610000000000000098, 0.3440000000000000280 ) ) ;
#7455=EDGE_CURVE ( 'NONE', #15103, #4834, #6486, .T. ) ;
#7481=DIRECTION ( 'NONE',  ( 0.000000000000000000, 1.000000000000000000, 0.000000000000000000 ) ) ;
#7492=ORIENTED_EDGE ( 'NONE', *, *, #11283, .F. ) ;
#7497=CARTESIAN_POINT ( 'NONE',  ( 0.000000000000000000, 1.109999999999999876, -0.2499999999999999167 ) ) ;
#7499=EDGE_LOOP ( 'NONE', ( #11286, #2511, #6832, #5552, #12540, #6536, #6833, #2799, #12055, #4257 ) ) ;
#7508=FACE_OUTER_BOUND ( 'NONE', #12901, .T. ) ;
#7517=AXIS2_PLACEMENT_3D ( 'NONE', #7948, #3437, #3210 ) ;
#7527=EDGE_LOOP ( 'NONE', ( #1837, #11194, #7492, #3183 ) ) ;
#7565=CARTESIAN_POINT ( 'NONE',  ( -0.2936128187763769604, 1.600826314462298283, -0.2533531860778197031 ) ) ;
#7567=VERTEX_POINT ( 'NONE', #5289 ) ;
#7568=ORIENTED_EDGE ( 'NONE', *, *, #1453, .F. ) ;
#7588=CARTESIAN_POINT ( 'NONE',  ( -0.4313007445438682974, 1.564783867144732277, 0.01487070305975445560 ) ) ;
#7599=ORIENTED_EDGE ( 'NONE', *, *, #3684, .T. ) ;
#7604=LINE ( 'NONE', #12265, #14521 ) ;
#7617=DIRECTION ( 'NONE',  ( 0.000000000000000000, 0.000000000000000000, -1.000000000000000000 ) ) ;
#7634=CARTESIAN_POINT ( 'NONE',  ( -0.4192535942842267049, 1.577705975193670840, -0.03573697939586736871 ) ) ;
#7674=( NAMED_UNIT ( * ) PLANE_ANGLE_UNIT ( ) SI_UNIT ( $, .RADIAN. ) );
#7700=CARTESIAN_POINT ( 'NONE',  ( 0.1787546228633458134, 1.577672892097735202, -0.3809527529760087239 ) ) ;
#7701=EDGE_LOOP ( 'NONE', ( #11648, #7232 ) ) ;
#7718=DIRECTION ( 'NONE',  ( -0.000000000000000000, -1.000000000000000000, -0.000000000000000000 ) ) ;
#7736=EDGE_LOOP ( 'NONE', ( #6982, #6684 ) ) ;
#7747=DIRECTION ( 'NONE',  ( -0.000000000000000000, -1.000000000000000000, -0.000000000000000000 ) ) ;
#7751=CARTESIAN_POINT ( 'NONE',  ( 0.4349147617188415249, 1.239999999999999991, 0.008611041693268213504 ) ) ;
#7768=AXIS2_PLACEMENT_3D ( 'NONE', #1735, #14374, #2829 ) ;
#7775=DIRECTION ( 'NONE',  ( 0.000000000000000000, 1.000000000000000000, 0.000000000000000000 ) ) ;
#7778=CARTESIAN_POINT ( 'NONE',  ( 0.2027934381167127154, 1.564766993392023631, -0.3809527529760087239 ) ) ;
#7785=DIRECTION ( 'NONE',  ( 0.000000000000000000, 1.000000000000000000, 0.000000000000000000 ) ) ;
#7857=CARTESIAN_POINT ( 'NONE',  ( 0.2100000000000001865, 1.239999999999999991, -0.3809527529760087239 ) ) ;
#7883=CARTESIAN_POINT ( 'NONE',  ( 0.000000000000000000, 0.000000000000000000, 0.000000000000000000 ) ) ;
#7887=EDGE_LOOP ( 'NONE', ( #1196, #7568, #9147, #10350 ) ) ;
#7928=CIRCLE ( 'NONE', #10627, 0.4849999999999999312 ) ;
#7948=CARTESIAN_POINT ( 'NONE',  ( 0.000000000000000000, 1.503199999999999870, -0.3439999999999999170 ) ) ;
#7990=ORIENTED_EDGE ( 'NONE', *, *, #9786, .F. ) ;
#8002=ORIENTED_EDGE ( 'NONE', *, *, #10501, .F. ) ;
#8008=CARTESIAN_POINT ( 'NONE',  ( 0.1444275314249800213, 1.589819979576903686, -0.3809527529760087239 ) ) ;
#8017=CIRCLE ( 'NONE', #1401, 0.4349999999999999978 ) ;
#8049=VECTOR ( 'NONE', #11023, 39.37007874015748854 ) ;
#8056=ORIENTED_EDGE ( 'NONE', *, *, #7330, .T. ) ;
#8061=ORIENTED_EDGE ( 'NONE', *, *, #10749, .F. ) ;
#8085=ORIENTED_EDGE ( 'NONE', *, *, #5375, .F. ) ;
#8107=ORIENTED_EDGE ( 'NONE', *, *, #7330, .F. ) ;
#8110=DIRECTION ( 'NONE',  ( 0.000000000000000000, 1.000000000000000000, 0.000000000000000000 ) ) ;
#8166=CARTESIAN_POINT ( 'NONE',  ( 0.3480879174158137412, 1.602949672542214321, -0.1589995474869895786 ) ) ;
#8171=CYLINDRICAL_SURFACE ( 'NONE', #10252, 0.2499999999999999167 ) ;
#8190=CARTESIAN_POINT ( 'NONE',  ( -0.009170202274341012275, 1.603403463250997696, -0.3809527529760086684 ) ) ;
#8195=EDGE_CURVE ( 'NONE', #6222, #3130, #6884, .T. ) ;
#8212=CARTESIAN_POINT ( 'NONE',  ( 0.000000000000000000, 1.109999999999999876, 0.000000000000000000 ) ) ;
#8239=B_SPLINE_CURVE_WITH_KNOTS ( 'NONE', 3,
 ( #14959, #632, #5329, #14658, #11216, #14729, #713, #4259, #6939, #3648, #11826, #3567, #8166, #8248, #4875, #5870, #14186, #2257, #12656, #2183, #1099, #4641 ),
 .UNSPECIFIED., .F., .F.,
 ( 4, 2, 2, 2, 2, 2, 2, 2, 2, 2, 4 ),
 ( 2.884201056608390597E-07, 0.0006930185370336857482, 0.001385748653961710536, 0.002771208887817760546, 0.004156669121673812507, 0.005542129355529864902, 0.006927589589385916430, 0.008313049823241968825, 0.009698510057098019485, 0.01039124017402604135, 0.01108397029095406494 ),
 .UNSPECIFIED. ) ;
#8248=CARTESIAN_POINT ( 'NONE',  ( 0.3662167046612953003, 1.600826314462299838, -0.1275995668982097264 ) ) ;
#8250=CARTESIAN_POINT ( 'NONE',  ( 0.2099999999999999922, 0.7512260236060024354, -0.3809527529760087239 ) ) ;
#8274=DIRECTION ( 'NONE',  ( 0.5000000000000041078, 0.000000000000000000, 0.8660254037844363761 ) ) ;
#8314=DIRECTION ( 'NONE',  ( 0.000000000000000000, 0.000000000000000000, -1.000000000000000000 ) ) ;
#8317=CIRCLE ( 'NONE', #5360, 0.4349999999999999978 ) ;
#8322=PLANE ( 'NONE',  #14070 ) ;
#8396=ORIENTED_EDGE ( 'NONE', *, *, #13397, .F. ) ;
#8401=EDGE_CURVE ( 'NONE', #15103, #3470, #9871, .T. ) ;
#8424=AXIS2_PLACEMENT_3D ( 'NONE', #5062, #7358, #1521 ) ;
#8467=FACE_OUTER_BOUND ( 'NONE', #12809, .T. ) ;
#8516=EDGE_CURVE ( 'NONE', #5884, #7375, #5038, .T. ) ;
#8518=DIRECTION ( 'NONE',  ( -0.5000000000000101030, 0.000000000000000000, -0.8660254037844328234 ) ) ;
#8521=VERTEX_POINT ( 'NONE', #3257 ) ;
#8527=CARTESIAN_POINT ( 'NONE',  ( -0.4193214606628511976, 1.577645543303436648, 0.03561943137996692599 ) ) ;
#8539=DIMENSIONAL_EXPONENTS ( 1.000000000000000000, 0.000000000000000000, 0.000000000000000000, 0.000000000000000000, 0.000000000000000000, 0.000000000000000000, 0.000000000000000000 ) ;
#8552=AXIS2_PLACEMENT_3D ( 'NONE', #9285, #13921, #13761 ) ;
#8558=EDGE_LOOP ( 'NONE', ( #2050, #476, #12320, #8754 ) ) ;
#8598=B_SPLINE_CURVE_WITH_KNOTS ( 'NONE', 3,
 ( #14732, #6705, #787, #951, #9082, #4486, #8008, #14963, #7700, #5562, #7778, #6561 ),
 .UNSPECIFIED., .F., .F.,
 ( 4, 2, 2, 2, 2, 4 ),
 ( 0.000000000000000000, 0.001383149773560842519, 0.002766299547121684604, 0.004149449320682526039, 0.004841024207462948925, 0.005532599094243372678 ),
 .UNSPECIFIED. ) ;
#8621=CARTESIAN_POINT ( 'NONE',  ( 4.665325695584414469E-17, 1.603403463250997918, 0.3809527529760087239 ) ) ;
#8632=CARTESIAN_POINT ( 'NONE',  ( 0.000000000000000000, 0.04580000000000046534, 0.000000000000000000 ) ) ;
#8663=PLANE ( 'NONE',  #2432 ) ;
#8664=EDGE_CURVE ( 'NONE', #3743, #5835, #8239, .T. ) ;
#8690=ORIENTED_EDGE ( 'NONE', *, *, #1286, .T. ) ;
#8720=AXIS2_PLACEMENT_3D ( 'NONE', #4733, #6117, #4660 ) ;
#8722=DIRECTION ( 'NONE',  ( 0.4999999999999979461, 0.000000000000000000, -0.8660254037844397068 ) ) ;
#8728=LINE ( 'NONE', #1683, #9998 ) ;
#8737=CARTESIAN_POINT ( 'NONE',  ( -0.3208433835780875043, 1.603403919227001762, 0.2061884643224599079 ) ) ;
#8754=ORIENTED_EDGE ( 'NONE', *, *, #1210, .T. ) ;
#8773=VECTOR ( 'NONE', #3948, 39.37007874015748143 ) ;
#8775=CARTESIAN_POINT ( 'NONE',  ( 0.09057123220595271473, 1.599173898159329976, 0.3809527529760087239 ) ) ;
#8776=FACE_OUTER_BOUND ( 'NONE', #3605, .T. ) ;
#8791=ORIENTED_EDGE ( 'NONE', *, *, #6387, .F. ) ;
#8834=FACE_OUTER_BOUND ( 'NONE', #14538, .T. ) ;
#8855=ADVANCED_FACE ( 'NONE', ( #3791 ), #6391, .F. ) ;
#8883=ADVANCED_FACE ( 'NONE', ( #8467 ), #1870, .T. ) ;
#8890=ORIENTED_EDGE ( 'NONE', *, *, #14840, .T. ) ;
#8908=ORIENTED_EDGE ( 'NONE', *, *, #3630, .F. ) ;
#8941=DIRECTION ( 'NONE',  ( -0.000000000000000000, -1.000000000000000000, -0.000000000000000000 ) ) ;
#8967=VECTOR ( 'NONE', #7775, 39.37007874015748143 ) ;
#9042=CARTESIAN_POINT ( 'NONE',  ( -0.2100000000000000200, 1.559103846021539619, -0.3809527529760087239 ) ) ;
#9050=EDGE_CURVE ( 'NONE', #4182, #6222, #1076, .T. ) ;
#9074=UNCERTAINTY_MEASURE_WITH_UNIT (LENGTH_MEASURE( 1.000000000000000082E-05 ), #5199, 'distance_accuracy_value', 'NONE');
#9082=CARTESIAN_POINT ( 'NONE',  ( 0.09067304051454581904, 1.599165379501958473, -0.3809527529760087239 ) ) ;
#9087=AXIS2_PLACEMENT_3D ( 'NONE', #3872, #7324, #13184 ) ;
#9097=DIRECTION ( 'NONE',  ( 0.000000000000000000, 0.000000000000000000, -1.000000000000000000 ) ) ;
#9118=EDGE_CURVE ( 'NONE', #8521, #6113, #7604, .T. ) ;
#9122=DIRECTION ( 'NONE',  ( 0.000000000000000000, 0.000000000000000000, -1.000000000000000000 ) ) ;
#9139=DIRECTION ( 'NONE',  ( 0.000000000000000000, 0.000000000000000000, -1.000000000000000000 ) ) ;
#9147=ORIENTED_EDGE ( 'NONE', *, *, #519, .T. ) ;
#9150=CARTESIAN_POINT ( 'NONE',  ( -0.2285287788938155373, 1.564783867144732499, -0.3660820499162559805 ) ) ;
#9156=CARTESIAN_POINT ( 'NONE',  ( -0.2027934381167096622, 1.564766993392025407, 0.3809527529760086684 ) ) ;
#9164=EDGE_CURVE ( 'NONE', #15007, #4210, #7928, .T. ) ;
#9177=FACE_OUTER_BOUND ( 'NONE', #14696, .T. ) ;
#9206=ORIENTED_EDGE ( 'NONE', *, *, #10876, .F. ) ;
#9222=EDGE_CURVE ( 'NONE', #9230, #7567, #14517, .T. ) ;
#9230=VERTEX_POINT ( 'NONE', #10028 ) ;
#9274=ADVANCED_FACE ( 'NONE', ( #6501 ), #1811, .T. ) ;
#9285=CARTESIAN_POINT ( 'NONE',  ( 0.000000000000000000, 1.610000000000000098, 0.000000000000000000 ) ) ;
#9290=AXIS2_PLACEMENT_3D ( 'NONE', #10403, #9414, #49 ) ;
#9300=FACE_BOUND ( 'NONE', #7736, .T. ) ;
#9303=DIRECTION ( 'NONE',  ( -0.000000000000000000, -1.000000000000000000, -0.000000000000000000 ) ) ;
#9401=EDGE_LOOP ( 'NONE', ( #9206, #3736 ) ) ;
#9402=CARTESIAN_POINT ( 'NONE',  ( 0.3208174396730070210, 1.603403006623434601, 0.2062334004842066582 ) ) ;
#9403=ORIENTED_EDGE ( 'NONE', *, *, #9784, .T. ) ;
#9412=LINE ( 'NONE', #10779, #3861 ) ;
#9414=DIRECTION ( 'NONE',  ( -0.000000000000000000, -1.000000000000000000, -0.000000000000000000 ) ) ;
#9420=VECTOR ( 'NONE', #322, 39.37007874015748143 ) ;
#9437=CARTESIAN_POINT ( 'NONE',  ( 0.000000000000000000, 1.109999999999999876, -0.4850000000000000977 ) ) ;
#9461=EDGE_LOOP ( 'NONE', ( #9766, #8890, #2158, #6134 ) ) ;
#9473=DIRECTION ( 'NONE',  ( 0.5000000000000101030, 0.000000000000000000, 0.8660254037844328234 ) ) ;
#9478=CARTESIAN_POINT ( 'NONE',  ( 0.4273790000700227187, 1.569549437900746636, 0.02166336374275166718 ) ) ;
#9485=PLANE ( 'NONE',  #6734 ) ;
#9490=B_SPLINE_CURVE_WITH_KNOTS ( 'NONE', 3,
 ( #13594, #7342, #4901, #10702, #195, #3509, #1503, #119, #11920, #1204, #4819, #11703, #8190, #5896 ),
 .UNSPECIFIED., .F., .F.,
 ( 4, 2, 2, 2, 2, 2, 4 ),
 ( 0.02339532894303463992, 0.02409265248687550084, 0.02478997603071635830, 0.02618462311839807322, 0.02757927020607978813, 0.02827659374992064559, 0.02897391729376150304 ),
 .UNSPECIFIED. ) ;
#9530=EDGE_CURVE ( 'NONE', #392, #6113, #836, .T. ) ;
#9563=FACE_OUTER_BOUND ( 'NONE', #7527, .T. ) ;
#9587=CARTESIAN_POINT ( 'NONE',  ( 0.000000000000000000, 1.239999999999999991, 0.000000000000000000 ) ) ;
#9640=ADVANCED_FACE ( 'NONE', ( #9563 ), #9485, .F. ) ;
#9686=CARTESIAN_POINT ( 'NONE',  ( 0.2099999999999999922, 0.7512260236060024354, 0.3809527529760087239 ) ) ;
#9697=CARTESIAN_POINT ( 'NONE',  ( -0.4349147617188414694, 1.239999999999999991, -0.008611041693271251005 ) ) ;
#9725=DIRECTION ( 'NONE',  ( 0.000000000000000000, 0.000000000000000000, -1.000000000000000000 ) ) ;
#9740=CARTESIAN_POINT ( 'NONE',  ( -0.4021230921906706057, 1.589827634136291135, 0.06540787938107404942 ) ) ;
#9766=ORIENTED_EDGE ( 'NONE', *, *, #9222, .T. ) ;
#9771=DIRECTION ( 'NONE',  ( 0.000000000000000000, -1.000000000000000000, -0.000000000000000000 ) ) ;
#9784=EDGE_CURVE ( 'NONE', #13032, #2839, #8598, .T. ) ;
#9786=EDGE_CURVE ( 'NONE', #3470, #14655, #11316, .T. ) ;
#9792=ORIENTED_EDGE ( 'NONE', *, *, #5280, .T. ) ;
#9799=AXIS2_PLACEMENT_3D ( 'NONE', #5720, #2430, #9473 ) ;
#9807=MECHANICAL_DESIGN_GEOMETRIC_PRESENTATION_REPRESENTATION('',(#7373),#6893);
#9810=CARTESIAN_POINT ( 'NONE',  ( -0.3932619838309059368, 1.593633255602467713, 0.08075576927155943274 ) ) ;
#9867=CARTESIAN_POINT ( 'NONE',  ( -0.2099999999999999922, 1.239999999999999991, -0.3809527529760087239 ) ) ;
#9871=B_SPLINE_CURVE_WITH_KNOTS ( 'NONE', 3,
 ( #14574, #10990, #10771, #5177, #1423, #12059, #9920, #8775, #6182, #3955, #4103, #480, #7404, #8621 ),
 .UNSPECIFIED., .F., .F.,
 ( 4, 2, 2, 2, 2, 2, 4 ),
 ( 0.02339532894303460175, 0.02409265248687545574, 0.02478997603071630973, 0.02618462311839802464, 0.02757927020607973956, 0.02827659374992059355, 0.02897391729376145100 ),
 .UNSPECIFIED. ) ;
#9904=DIRECTION ( 'NONE',  ( 0.000000000000000000, 0.000000000000000000, 1.000000000000000000 ) ) ;
#9920=CARTESIAN_POINT ( 'NONE',  ( 0.1264631971972072777, 1.593677921218988880, 0.3809527529760087794 ) ) ;
#9939=CARTESIAN_POINT ( 'NONE',  ( -0.2405080627748324984, 1.577645543303435760, -0.3453333215960435187 ) ) ;
#9961=PRODUCT ( 'Hex Bolt', 'Hex Bolt', '', ( #10923 ) ) ;
#9975=FACE_OUTER_BOUND ( 'NONE', #14388, .T. ) ;
#9998=VECTOR ( 'NONE', #8518, 39.37007874015748143 ) ;
#10027=CARTESIAN_POINT ( 'NONE',  ( 0.000000000000000000, 1.239999999999999991, -0.4849999999999999312 ) ) ;
#10028=CARTESIAN_POINT ( 'NONE',  ( -0.2249147617188397563, 1.239999999999999991, 0.3723417112827376307 ) ) ;
#10060=CARTESIAN_POINT ( 'NONE',  ( 0.000000000000000000, 1.109999999999999876, 0.000000000000000000 ) ) ;
#10154=ORIENTED_EDGE ( 'NONE', *, *, #9164, .T. ) ;
#10250=CARTESIAN_POINT ( 'NONE',  ( 0.000000000000000000, 0.000000000000000000, 0.000000000000000000 ) ) ;
#10252=AXIS2_PLACEMENT_3D ( 'NONE', #11680, #1186, #14114 ) ;
#10293=ORIENTED_EDGE ( 'NONE', *, *, #4684, .T. ) ;
#10295=CARTESIAN_POINT ( 'NONE',  ( -0.4312750580175238602, 1.564824237736551771, -0.01491519342844984525 ) ) ;
#10299=CYLINDRICAL_SURFACE ( 'NONE', #6772, 0.4349999999999999423 ) ;
#10304=EDGE_CURVE ( 'NONE', #12746, #5546, #10738, .T. ) ;
#10307=DIRECTION ( 'NONE',  ( 0.000000000000000000, 0.000000000000000000, -1.000000000000000000 ) ) ;
#10350=ORIENTED_EDGE ( 'NONE', *, *, #2611, .F. ) ;
#10352=LINE ( 'NONE', #14011, #1784 ) ;
#10353=ORIENTED_EDGE ( 'NONE', *, *, #13537, .F. ) ;
#10403=CARTESIAN_POINT ( 'NONE',  ( 0.000000000000000000, 1.239999999999999991, 0.000000000000000000 ) ) ;
#10435=PLANE ( 'NONE',  #13305 ) ;
#10463=CARTESIAN_POINT ( 'NONE',  ( 0.3480941905909775147, 1.602948811930423156, 0.1589886820288792801 ) ) ;
#10469=EDGE_LOOP ( 'NONE', ( #8085, #8908, #13503, #3972 ) ) ;
#10481=VECTOR ( 'NONE', #14530, 39.37007874015748143 ) ;
#10501=EDGE_CURVE ( 'NONE', #6554, #39, #8317, .T. ) ;
#10511=DIRECTION ( 'NONE',  ( 0.000000000000000000, 1.000000000000000000, 0.000000000000000000 ) ) ;
#10541=CARTESIAN_POINT ( 'NONE',  ( 0.2285287788938192011, 1.564783867144734053, 0.3660820499162522612 ) ) ;
#10552=ADVANCED_FACE ( 'NONE', ( #10888 ), #8663, .F. ) ;
#10557=CARTESIAN_POINT ( 'NONE',  ( 0.2099999999999999922, 1.239999999999999991, 0.3809527529760087239 ) ) ;
#10581=DIRECTION ( 'NONE',  ( 0.000000000000000000, 0.000000000000000000, -1.000000000000000000 ) ) ;
#10599=CLOSED_SHELL ( 'NONE', ( #12057, #8883, #11682, #3633, #11312, #5493, #3011, #9640, #6533, #8855, #4691, #2776, #4752, #10991, #9274, #4194, #884, #3310, #6842, #4677, #10552, #4281, #14651, #10688 ) ) ;
#10615=ORIENTED_EDGE ( 'NONE', *, *, #11407, .F. ) ;
#10620=ORIENTED_EDGE ( 'NONE', *, *, #11283, .T. ) ;
#10627=AXIS2_PLACEMENT_3D ( 'NONE', #4467, #14226, #9139 ) ;
#10662=CARTESIAN_POINT ( 'NONE',  ( -0.4349147617188414694, 1.239999999999999991, -0.008611041693271251005 ) ) ;
#10688=ADVANCED_FACE ( 'NONE', ( #12853 ), #5752, .T. ) ;
#10702=CARTESIAN_POINT ( 'NONE',  ( -0.1786439721334353026, 1.577722767886655886, -0.3809527529760087239 ) ) ;
#10703=CYLINDRICAL_SURFACE ( 'NONE', #3157, 0.4349999999999999423 ) ;
#10719=CARTESIAN_POINT ( 'NONE',  ( -0.2099999999999999922, 0.7512260236060024354, -0.3809527529760087239 ) ) ;
#10720=( NAMED_UNIT ( * ) PLANE_ANGLE_UNIT ( ) SI_UNIT ( $, .RADIAN. ) );
#10724=DIRECTION ( 'NONE',  ( 0.000000000000000000, 0.000000000000000000, -1.000000000000000000 ) ) ;
#10738=LINE ( 'NONE', #12316, #10481 ) ;
#10748=DIRECTION ( 'NONE',  ( 0.000000000000000000, 0.000000000000000000, -1.000000000000000000 ) ) ;
#10749=EDGE_CURVE ( 'NONE', #710, #2919, #15139, .T. ) ;
#10757=EDGE_CURVE ( 'NONE', #2639, #2008, #1936, .T. ) ;
#10771=CARTESIAN_POINT ( 'NONE',  ( 0.1949587543783453114, 1.569534359386387967, 0.3809527529760087239 ) ) ;
#10779=CARTESIAN_POINT ( 'NONE',  ( -0.2249147617188397563, 1.239999999999999991, 0.3723417112827376307 ) ) ;
#10804=VECTOR ( 'NONE', #4795, 39.37007874015748143 ) ;
#10805=CYLINDRICAL_SURFACE ( 'NONE', #11798, 0.4850000000000000422 ) ;
#10831=CARTESIAN_POINT ( 'NONE',  ( 0.000000000000000000, 0.000000000000000000, -0.2499999999999999167 ) ) ;
#10832=CARTESIAN_POINT ( 'NONE',  ( 0.4349147617188408588, 1.559103846021540951, -0.008611041693278118775 ) ) ;
#10848=( GEOMETRIC_REPRESENTATION_CONTEXT ( 3 ) GLOBAL_UNCERTAINTY_ASSIGNED_CONTEXT ( ( #9074 ) ) GLOBAL_UNIT_ASSIGNED_CONTEXT ( ( #5199, #10720, #4916 ) ) REPRESENTATION_CONTEXT ( 'NONE', 'WORKASPACE' ) );
#10850=EDGE_CURVE ( 'NONE', #39, #15103, #1452, .T. ) ;
#10876=EDGE_CURVE ( 'NONE', #4210, #15007, #420, .T. ) ;
#10878=DIRECTION ( 'NONE',  ( 0.000000000000000000, 0.000000000000000000, -1.000000000000000000 ) ) ;
#10888=FACE_OUTER_BOUND ( 'NONE', #11608, .T. ) ;
#10923=PRODUCT_CONTEXT ( 'NONE', #7067, 'mechanical' ) ;
#10990=CARTESIAN_POINT ( 'NONE',  ( 0.2028461515626820422, 1.564725569476186795, 0.3809527529760088904 ) ) ;
#10991=ADVANCED_FACE ( 'NONE', ( #1674 ), #4055, .F. ) ;
#11009=ORIENTED_EDGE ( 'NONE', *, *, #822, .T. ) ;
#11012=CARTESIAN_POINT ( 'NONE',  ( -0.2249147617188397563, 0.7512260236060024354, 0.3723417112827376307 ) ) ;
#11023=DIRECTION ( 'NONE',  ( 8.659560562354914369E-17, 0.7071067811865490160, -0.7071067811865459074 ) ) ;
#11028=CARTESIAN_POINT ( 'NONE',  ( -0.2578780456881166749, 1.589927591219160385, 0.3152476286636298197 ) ) ;
#11058=DIRECTION ( 'NONE',  ( 0.000000000000000000, 1.000000000000000000, 0.000000000000000000 ) ) ;
#11079=DIRECTION ( 'NONE',  ( -0.000000000000000000, -1.000000000000000000, -0.000000000000000000 ) ) ;
#11091=ORIENTED_EDGE ( 'NONE', *, *, #12261, .F. ) ;
#11118=DIRECTION ( 'NONE',  ( 0.000000000000000000, 1.000000000000000000, 0.000000000000000000 ) ) ;
#11128=CARTESIAN_POINT ( 'NONE',  ( -0.2249147617188422543, 1.239999999999999991, -0.3723417112827361319 ) ) ;
#11180=EDGE_CURVE ( 'NONE', #2919, #3470, #15100, .T. ) ;
#11193=ORIENTED_EDGE ( 'NONE', *, *, #383, .T. ) ;
#11194=ORIENTED_EDGE ( 'NONE', *, *, #6907, .T. ) ;
#11210=B_SPLINE_CURVE_WITH_KNOTS ( 'NONE', 3,
 ( #2629, #4069, #525, #14319, #7439, #11028, #3992, #231, #6151, #7306, #8737, #4933, #3777, #5006, #5152, #9810, #9740, #12027, #8527, #3857, #7588, #11961 ),
 .UNSPECIFIED., .F., .F.,
 ( 4, 2, 2, 2, 2, 2, 2, 2, 2, 2, 4 ),
 ( 2.884201070676985282E-07, 0.0006930185370350131369, 0.001385748653962958453, 0.002771208887818838677, 0.004156669121674718900, 0.005542129355530598690, 0.006927589589386478480, 0.008313049823242359138, 0.009698510057098238060, 0.01039124017402617665, 0.01108397029095411178 ),
 .UNSPECIFIED. ) ;
#11216=CARTESIAN_POINT ( 'NONE',  ( 0.2448097035962774060, 1.581125151349147107, -0.3378826611373836886 ) ) ;
#11237=ORIENTED_EDGE ( 'NONE', *, *, #14195, .T. ) ;
#11241=SHAPE_REPRESENTATION_RELATIONSHIP ( 'NONE' , 'NONE' ,  #1600, #5839 ) ;
#11262=CARTESIAN_POINT ( 'NONE',  ( 0.000000000000000000, 1.239999999999999991, 0.000000000000000000 ) ) ;
#11268=DIRECTION ( 'NONE',  ( 0.4999999999999918954, 0.000000000000000000, -0.8660254037844431485 ) ) ;
#11283=EDGE_CURVE ( 'NONE', #6554, #4834, #14208, .T. ) ;
#11286=ORIENTED_EDGE ( 'NONE', *, *, #10749, .T. ) ;
#11300=ORIENTED_EDGE ( 'NONE', *, *, #8195, .F. ) ;
#11310=DIRECTION ( 'NONE',  ( 0.000000000000000000, 1.000000000000000000, 0.000000000000000000 ) ) ;
#11312=ADVANCED_FACE ( 'NONE', ( #4739 ), #10703, .T. ) ;
#11316=B_SPLINE_CURVE_WITH_KNOTS ( 'NONE', 3,
 ( #12439, #2100, #5483, #11448, #4188, #14811, #867, #3193, #4262, #5715, #9156, #2022 ),
 .UNSPECIFIED., .F., .F.,
 ( 4, 2, 2, 2, 2, 4 ),
 ( 3.848605514871169070E-18, 0.001383149773560821052, 0.002766299547121638201, 0.004149449320682454048, 0.004841024207462863924, 0.005532599094243272932 ),
 .UNSPECIFIED. ) ;
#11358=CARTESIAN_POINT ( 'NONE',  ( -0.4273790000699995706, 1.569549437900772393, -0.02166336374279465016 ) ) ;
#11392=AXIS2_PLACEMENT_3D ( 'NONE', #12416, #2321, #8314 ) ;
#11407=EDGE_CURVE ( 'NONE', #3130, #2748, #13640, .T. ) ;
#11413=CARTESIAN_POINT ( 'NONE',  ( 0.000000000000000000, 1.239999999999999991, 0.000000000000000000 ) ) ;
#11441=CARTESIAN_POINT ( 'NONE',  ( -0.4019514777495646340, 1.589927591219160830, -0.06570512431237962581 ) ) ;
#11445=FACE_OUTER_BOUND ( 'NONE', #11580, .T. ) ;
#11448=CARTESIAN_POINT ( 'NONE',  ( -0.07259084472369319030, 1.600827197418697390, 0.3809527529760087794 ) ) ;
#11462=ORIENTED_EDGE ( 'NONE', *, *, #5218, .F. ) ;
#11497=CARTESIAN_POINT ( 'NONE',  ( 2.781172880863636303E-17, 0.000000000000000000, -0.2041999999999996596 ) ) ;
#11538=DIRECTION ( 'NONE',  ( -0.000000000000000000, -1.000000000000000000, -0.000000000000000000 ) ) ;
#11561=ORIENTED_EDGE ( 'NONE', *, *, #8516, .T. ) ;
#11580=EDGE_LOOP ( 'NONE', ( #177, #3854, #4927, #10293 ) ) ;
#11608=EDGE_LOOP ( 'NONE', ( #1367, #7599, #9403, #1094, #246 ) ) ;
#11619=CARTESIAN_POINT ( 'NONE',  ( 0.4349147617188415249, 0.7512260236060024354, 0.008611041693268213504 ) ) ;
#11633=CARTESIAN_POINT ( 'NONE',  ( 0.2249147617188448078, 1.239999999999999991, 0.3723417112827345221 ) ) ;
#11648=ORIENTED_EDGE ( 'NONE', *, *, #1453, .T. ) ;
#11650=CARTESIAN_POINT ( 'NONE',  ( 0.000000000000000000, 1.610000000000000098, -0.3440000000000000280 ) ) ;
#11680=CARTESIAN_POINT ( 'NONE',  ( 0.000000000000000000, 0.000000000000000000, 0.000000000000000000 ) ) ;
#11682=ADVANCED_FACE ( 'NONE', ( #4720 ), #8171, .T. ) ;
#11703=CARTESIAN_POINT ( 'NONE',  ( -0.01817859877509239372, 1.603284996591855194, -0.3809527529760087239 ) ) ;
#11739=CARTESIAN_POINT ( 'NONE',  ( 0.000000000000000000, 1.559103846021539619, 0.000000000000000000 ) ) ;
#11798=AXIS2_PLACEMENT_3D ( 'NONE', #3848, #5213, #10878 ) ;
#11826=CARTESIAN_POINT ( 'NONE',  ( 0.3208433835780706289, 1.603403919227001539, -0.2061884643224887181 ) ) ;
#11836=CARTESIAN_POINT ( 'NONE',  ( 0.4312750580175467308, 1.564824237736521351, 0.01491519342840733238 ) ) ;
#11843=PRODUCT_DEFINITION_FORMATION_WITH_SPECIFIED_SOURCE ( 'ANY', '', #9961, .NOT_KNOWN. ) ;
#11885=EDGE_LOOP ( 'NONE', ( #11300, #6353, #13201, #7336 ) ) ;
#11909=ORIENTED_EDGE ( 'NONE', *, *, #14769, .T. ) ;
#11920=CARTESIAN_POINT ( 'NONE',  ( -0.07252880680210840869, 1.600831684639946184, -0.3809527529760086684 ) ) ;
#11942=DIRECTION ( 'NONE',  ( 0.000000000000000000, 1.000000000000000000, 0.000000000000000000 ) ) ;
#11956=VECTOR ( 'NONE', #13203, 39.37007874015748143 ) ;
#11961=CARTESIAN_POINT ( 'NONE',  ( -0.4349147617188414139, 1.559103846021539619, 0.008611041693274201769 ) ) ;
#11993=ORIENTED_EDGE ( 'NONE', *, *, #5030, .T. ) ;
#12027=CARTESIAN_POINT ( 'NONE',  ( -0.4150689297652816467, 1.581084130983675617, 0.04298503095531345380 ) ) ;
#12039=DIRECTION ( 'NONE',  ( -0.000000000000000000, -1.000000000000000000, -0.000000000000000000 ) ) ;
#12055=ORIENTED_EDGE ( 'NONE', *, *, #9784, .F. ) ;
#12057=ADVANCED_FACE ( 'NONE', ( #7234 ), #14895, .T. ) ;
#12059=CARTESIAN_POINT ( 'NONE',  ( 0.1444440947987239432, 1.589814529920261954, 0.3809527529760087239 ) ) ;
#12080=FACE_OUTER_BOUND ( 'NONE', #9401, .T. ) ;
#12082=EDGE_LOOP ( 'NONE', ( #12673, #14709, #155, #5844, #6650, #7158, #2177, #6120, #12703, #5993, #2548, #15030 ) ) ;
#12105=CARTESIAN_POINT ( 'NONE',  ( -0.2249147617188422821, 1.559103846021539619, -0.3723417112827360209 ) ) ;
#12196=AXIS2_PLACEMENT_3D ( 'NONE', #12773, #2144, #5679 ) ;
#12219=CARTESIAN_POINT ( 'NONE',  ( 5.939536975864664694E-17, 1.109999999999999876, 0.4850000000000001532 ) ) ;
#12226=CARTESIAN_POINT ( 'NONE',  ( -0.2324059764400444317, 1.569496918332967228, -0.3593665467752061304 ) ) ;
#12230=PLANE ( 'NONE',  #7768 ) ;
#12232=ORIENTED_EDGE ( 'NONE', *, *, #9530, .T. ) ;
#12261=EDGE_CURVE ( 'NONE', #1386, #9230, #1207, .T. ) ;
#12265=CARTESIAN_POINT ( 'NONE',  ( -0.4349147617188414694, 0.7512260236060024354, 0.008611041693274290240 ) ) ;
#12281=DIRECTION ( 'NONE',  ( -0.8660254037844433705, 0.000000000000000000, -0.4999999999999920064 ) ) ;
#12296=CARTESIAN_POINT ( 'NONE',  ( -0.3117416060218557994, 1.602949672542212989, -0.2219532054890435979 ) ) ;
#12316=CARTESIAN_POINT ( 'NONE',  ( 0.4349147617188415249, 0.7512260236060024354, 0.008611041693268213504 ) ) ;
#12320=ORIENTED_EDGE ( 'NONE', *, *, #4050, .F. ) ;
#12396=CARTESIAN_POINT ( 'NONE',  ( -0.2099999999999999922, 1.239999999999999991, -0.3809527529760087239 ) ) ;
#12401=CONICAL_SURFACE ( 'NONE', #1161, 0.2041999999999996596, 0.7853981633974460586 ) ;
#12411=AXIS2_PLACEMENT_3D ( 'NONE', #12687, #12525, #15141 ) ;
#12416=CARTESIAN_POINT ( 'NONE',  ( 0.000000000000000000, 1.503199999999999870, 0.000000000000000000 ) ) ;
#12439=CARTESIAN_POINT ( 'NONE',  ( 4.665325695584414469E-17, 1.603403463250997918, 0.3809527529760087239 ) ) ;
#12443=DIRECTION ( 'NONE',  ( 6.483702463810914196E-14, 0.000000000000000000, -1.000000000000000000 ) ) ;
#12525=DIRECTION ( 'NONE',  ( 1.000000000000000000, 0.000000000000000000, -1.224646799147353207E-16 ) ) ;
#12540=ORIENTED_EDGE ( 'NONE', *, *, #6907, .F. ) ;
#12542=DIRECTION ( 'NONE',  ( 0.000000000000000000, 0.000000000000000000, -1.000000000000000000 ) ) ;
#12550=CIRCLE ( 'NONE', #14506, 0.4349999999999999423 ) ;
#12564=AXIS2_PLACEMENT_3D ( 'NONE', #14635, #12039, #462 ) ;
#12587=CARTESIAN_POINT ( 'NONE',  ( -0.4349147617188193760, 1.559103846021574480, -0.008611041693309614414 ) ) ;
#12612=DIRECTION ( 'NONE',  ( -0.000000000000000000, -1.000000000000000000, -0.000000000000000000 ) ) ;
#12624=VECTOR ( 'NONE', #5480, 39.37007874015748854 ) ;
#12641=CARTESIAN_POINT ( 'NONE',  ( 0.4850000000000000977, 1.109999999999999876, 0.000000000000000000 ) ) ;
#12656=CARTESIAN_POINT ( 'NONE',  ( 0.4193214606628480889, 1.577645543303439313, -0.03561943137997464898 ) ) ;
#12673=ORIENTED_EDGE ( 'NONE', *, *, #1938, .T. ) ;
#12687=CARTESIAN_POINT ( 'NONE',  ( 4.212784989066894333E-17, 1.503199999999999870, 0.3439999999999999170 ) ) ;
#12703=ORIENTED_EDGE ( 'NONE', *, *, #4311, .T. ) ;
#12706=DIRECTION ( 'NONE',  ( 0.000000000000000000, 0.000000000000000000, -1.000000000000000000 ) ) ;
#12712=ORIENTED_EDGE ( 'NONE', *, *, #14840, .F. ) ;
#12719=DIRECTION ( 'NONE',  ( 0.000000000000000000, 0.000000000000000000, -1.000000000000000000 ) ) ;
#12742=CARTESIAN_POINT ( 'NONE',  ( 0.4349147617188415249, 1.559103846021539619, 0.008611041693268213504 ) ) ;
#12744=VERTEX_POINT ( 'NONE', #7857 ) ;
#12746=VERTEX_POINT ( 'NONE', #1030 ) ;
#12748=VECTOR ( 'NONE', #3924, 39.37007874015748143 ) ;
#12773=CARTESIAN_POINT ( 'NONE',  ( 0.000000000000000000, 1.610000000000000098, 0.000000000000000000 ) ) ;
#12796=AXIS2_PLACEMENT_3D ( 'NONE', #13447, #14604, #5364 ) ;
#12809=EDGE_LOOP ( 'NONE', ( #11462, #8690, #10615, #6445 ) ) ;
#12821=CARTESIAN_POINT ( 'NONE',  ( 0.2324059764400484562, 1.569496918332968782, 0.3593665467752015230 ) ) ;
#12836=CARTESIAN_POINT ( 'NONE',  ( -0.4349147617188414139, 1.559103846021539619, 0.008611041693274201769 ) ) ;
#12848=AXIS2_PLACEMENT_3D ( 'NONE', #8632, #7413, #13276 ) ;
#12853=FACE_OUTER_BOUND ( 'NONE', #4225, .T. ) ;
#12855=VECTOR ( 'NONE', #11538, 39.37007874015748143 ) ;
#12876=EDGE_CURVE ( 'NONE', #4182, #2748, #6171, .T. ) ;
#12901=EDGE_LOOP ( 'NONE', ( #10353, #10154, #11009, #2565 ) ) ;
#12947=LINE ( 'NONE', #154, #358 ) ;
#12954=CARTESIAN_POINT ( 'NONE',  ( -0.2249147617188397563, 0.7512260236060024354, 0.3723417112827376307 ) ) ;
#12983=CARTESIAN_POINT ( 'NONE',  ( 0.2249147617188371751, 1.559103846021539619, -0.3723417112827391295 ) ) ;
#13023=FACE_OUTER_BOUND ( 'NONE', #9461, .T. ) ;
#13032=VERTEX_POINT ( 'NONE', #13712 ) ;
#13085=CARTESIAN_POINT ( 'NONE',  ( 0.000000000000000000, 0.000000000000000000, -0.4850000000000000422 ) ) ;
#13113=AXIS2_PLACEMENT_3D ( 'NONE', #9686, #1624, #14256 ) ;
#13128=ORIENTED_EDGE ( 'NONE', *, *, #6387, .T. ) ;
#13180=ORIENTED_EDGE ( 'NONE', *, *, #9118, .T. ) ;
#13184=DIRECTION ( 'NONE',  ( 0.000000000000000000, 0.000000000000000000, -1.000000000000000000 ) ) ;
#13201=ORIENTED_EDGE ( 'NONE', *, *, #12876, .T. ) ;
#13203=DIRECTION ( 'NONE',  ( 0.000000000000000000, 1.000000000000000000, 0.000000000000000000 ) ) ;
#13206=VECTOR ( 'NONE', #11268, 39.37007874015748854 ) ;
#13211=EDGE_LOOP ( 'NONE', ( #7102, #1202, #809, #6011 ) ) ;
#13214=VERTEX_POINT ( 'NONE', #12105 ) ;
#13216=FACE_OUTER_BOUND ( 'NONE', #7887, .T. ) ;
#13276=DIRECTION ( 'NONE',  ( 0.000000000000000000, 0.000000000000000000, -1.000000000000000000 ) ) ;
#13302=AXIS2_PLACEMENT_3D ( 'NONE', #3208, #8110, #1893 ) ;
#13305=AXIS2_PLACEMENT_3D ( 'NONE', #12641, #6854, #12719 ) ;
#13343=EDGE_LOOP ( 'NONE', ( #5500, #13601, #3689, #1894, #11909 ) ) ;
#13357=CARTESIAN_POINT ( 'NONE',  ( -0.4150198198413779238, 1.581125151349165758, -0.04307009183866805646 ) ) ;
#13363=CARTESIAN_POINT ( 'NONE',  ( 0.000000000000000000, 0.000000000000000000, 0.000000000000000000 ) ) ;
#13383=VECTOR ( 'NONE', #11942, 39.37007874015748143 ) ;
#13397=EDGE_CURVE ( 'NONE', #2101, #12746, #13784, .T. ) ;
#13421=CARTESIAN_POINT ( 'NONE',  ( 0.000000000000000000, 0.000000000000000000, 0.000000000000000000 ) ) ;
#13425=EDGE_LOOP ( 'NONE', ( #15060, #13868, #8396, #1121 ) ) ;
#13447=CARTESIAN_POINT ( 'NONE',  ( 0.000000000000000000, 1.559103846021539619, 0.000000000000000000 ) ) ;
#13466=CIRCLE ( 'NONE', #9087, 0.4850000000000000977 ) ;
#13468=ORIENTED_EDGE ( 'NONE', *, *, #10757, .T. ) ;
#13503=ORIENTED_EDGE ( 'NONE', *, *, #1938, .F. ) ;
#13537=EDGE_CURVE ( 'NONE', #15007, #2639, #3533, .T. ) ;
#13594=CARTESIAN_POINT ( 'NONE',  ( -0.2100000000000000200, 1.559103846021539619, -0.3809527529760087239 ) ) ;
#13601=ORIENTED_EDGE ( 'NONE', *, *, #8401, .T. ) ;
#13640=CIRCLE ( 'NONE', #3884, 0.2499999999999999167 ) ;
#13712=CARTESIAN_POINT ( 'NONE',  ( 0.000000000000000000, 1.603403463250997918, -0.3809527529760087239 ) ) ;
#13718=ORIENTED_EDGE ( 'NONE', *, *, #3667, .T. ) ;
#13761=DIRECTION ( 'NONE',  ( 0.000000000000000000, 0.000000000000000000, -1.000000000000000000 ) ) ;
#13770=VERTEX_POINT ( 'NONE', #9042 ) ;
#13771=VECTOR ( 'NONE', #14683, 39.37007874015748143 ) ;
#13784=CIRCLE ( 'NONE', #6985, 0.4349999999999999978 ) ;
#13862=AXIS2_PLACEMENT_3D ( 'NONE', #11413, #7747, #915 ) ;
#13868=ORIENTED_EDGE ( 'NONE', *, *, #10304, .F. ) ;
#13888=CARTESIAN_POINT ( 'NONE',  ( 0.3662050505264397016, 1.600827805288693062, 0.1276197524518947191 ) ) ;
#13921=DIRECTION ( 'NONE',  ( -0.000000000000000000, -1.000000000000000000, -0.000000000000000000 ) ) ;
#13976=AXIS2_PLACEMENT_3D ( 'NONE', #15048, #7114, #14969 ) ;
#14011=CARTESIAN_POINT ( 'NONE',  ( 0.2099999999999999922, 1.239999999999999991, 0.3809527529760087239 ) ) ;
#14070=AXIS2_PLACEMENT_3D ( 'NONE', #12954, #4634, #1167 ) ;
#14071=TOROIDAL_SURFACE ( 'NONE', #11392, 0.3439999999999999170, 0.1068000000000000754 ) ;
#14104=AXIS2_PLACEMENT_3D ( 'NONE', #10250, #2123, #810 ) ;
#14114=DIRECTION ( 'NONE',  ( 0.000000000000000000, 0.000000000000000000, -1.000000000000000000 ) ) ;
#14118=AXIS2_PLACEMENT_3D ( 'NONE', #886, #966, #806 ) ;
#14125=CARTESIAN_POINT ( 'NONE',  ( 0.3117416060218692886, 1.602949672542214321, 0.2219532054890206441 ) ) ;
#14155=CARTESIAN_POINT ( 'NONE',  ( 0.4349147617188413584, 0.7512260236060024354, -0.008611041693277364170 ) ) ;
#14186=CARTESIAN_POINT ( 'NONE',  ( 0.4021230921906648881, 1.589827634136293577, -0.06540787938108565125 ) ) ;
#14190=AXIS2_PLACEMENT_3D ( 'NONE', #3121, #7785, #12443 ) ;
#14195=EDGE_CURVE ( 'NONE', #392, #13214, #4114, .T. ) ;
#14208=LINE ( 'NONE', #3594, #11956 ) ;
#14226=DIRECTION ( 'NONE',  ( -0.000000000000000000, -1.000000000000000000, -0.000000000000000000 ) ) ;
#14235=CARTESIAN_POINT ( 'NONE',  ( 2.500728763858891129E-17, 0.000000000000000000, -0.2041999999999996596 ) ) ;
#14252=ORIENTED_EDGE ( 'NONE', *, *, #5030, .F. ) ;
#14256=DIRECTION ( 'NONE',  ( -1.000000000000000000, 0.000000000000000000, 0.000000000000000000 ) ) ;
#14298=LINE ( 'NONE', #10719, #655 ) ;
#14319=CARTESIAN_POINT ( 'NONE',  ( -0.2405759291534545763, 1.577705975193670840, 0.3452157735801421046 ) ) ;
#14334=DIRECTION ( 'NONE',  ( 0.000000000000000000, 1.000000000000000000, 0.000000000000000000 ) ) ;
#14357=VECTOR ( 'NONE', #1143, 39.37007874015748143 ) ;
#14374=DIRECTION ( 'NONE',  ( 0.000000000000000000, 1.000000000000000000, 0.000000000000000000 ) ) ;
#14388=EDGE_LOOP ( 'NONE', ( #14624, #1927, #8002, #10620 ) ) ;
#14416=CARTESIAN_POINT ( 'NONE',  ( 0.000000000000000000, 0.000000000000000000, 0.000000000000000000 ) ) ;
#14506=AXIS2_PLACEMENT_3D ( 'NONE', #7278, #1441, #6130 ) ;
#14508=CARTESIAN_POINT ( 'NONE',  ( 0.000000000000000000, 0.000000000000000000, 0.2041999999999996596 ) ) ;
#14517=LINE ( 'NONE', #11012, #13771 ) ;
#14521=VECTOR ( 'NONE', #11118, 39.37007874015748143 ) ;
#14528=LINE ( 'NONE', #14235, #8049 ) ;
#14530=DIRECTION ( 'NONE',  ( 0.000000000000000000, 1.000000000000000000, 0.000000000000000000 ) ) ;
#14538=EDGE_LOOP ( 'NONE', ( #6551, #11193, #13718, #1118, #9792, #3834, #12232, #12712, #13128, #7990 ) ) ;
#14574=CARTESIAN_POINT ( 'NONE',  ( 0.2099999999999999922, 1.559103846021539619, 0.3809527529760087239 ) ) ;
#14594=CARTESIAN_POINT ( 'NONE',  ( -0.2249147617188422821, 1.559103846021539619, -0.3723417112827360209 ) ) ;
#14604=DIRECTION ( 'NONE',  ( 0.000000000000000000, 1.000000000000000000, 0.000000000000000000 ) ) ;
#14610=DIRECTION ( 'NONE',  ( -0.000000000000000000, -1.000000000000000000, -0.000000000000000000 ) ) ;
#14622=AXIS2_PLACEMENT_3D ( 'NONE', #811, #1814, #8722 ) ;
#14624=ORIENTED_EDGE ( 'NONE', *, *, #7455, .F. ) ;
#14635=CARTESIAN_POINT ( 'NONE',  ( 0.000000000000000000, 0.000000000000000000, 0.000000000000000000 ) ) ;
#14641=ORIENTED_EDGE ( 'NONE', *, *, #9530, .F. ) ;
#14651=ADVANCED_FACE ( 'NONE', ( #8834 ), #14071, .T. ) ;
#14655=VERTEX_POINT ( 'NONE', #7231 ) ;
#14658=CARTESIAN_POINT ( 'NONE',  ( 0.2405759291534288191, 1.577705975193649968, -0.3452157735801837934 ) ) ;
#14674=CYLINDRICAL_SURFACE ( 'NONE', #1777, 0.2499999999999999167 ) ;
#14683=DIRECTION ( 'NONE',  ( 0.000000000000000000, 1.000000000000000000, 0.000000000000000000 ) ) ;
#14696=EDGE_LOOP ( 'NONE', ( #5977, #15090, #14252, #6330 ) ) ;
#14709=ORIENTED_EDGE ( 'NONE', *, *, #1210, .F. ) ;
#14729=CARTESIAN_POINT ( 'NONE',  ( 0.2578780456880921390, 1.589927591219149949, -0.3152476286636705649 ) ) ;
#14732=CARTESIAN_POINT ( 'NONE',  ( 0.000000000000000000, 1.603403463250997918, -0.3809527529760087239 ) ) ;
#14769=EDGE_CURVE ( 'NONE', #1386, #39, #10352, .T. ) ;
#14808=LINE ( 'NONE', #14888, #8967 ) ;
#14811=CARTESIAN_POINT ( 'NONE',  ( -0.1266950372298287220, 1.593635284016129194, 0.3809527529760087239 ) ) ;
#14840=EDGE_CURVE ( 'NONE', #7567, #6113, #11210, .T. ) ;
#14842=FACE_OUTER_BOUND ( 'NONE', #676, .T. ) ;
#14885=CARTESIAN_POINT ( 'NONE',  ( -0.3389861398595948039, 1.603403919227001762, -0.1747642886535499263 ) ) ;
#14888=CARTESIAN_POINT ( 'NONE',  ( -0.2099999999999999922, 0.7512260236060024354, 0.3809527529760087239 ) ) ;
#14895=TOROIDAL_SURFACE ( 'NONE', #5134, 0.3439999999999999170, 0.1068000000000000754 ) ;
#14900=VERTEX_POINT ( 'NONE', #12396 ) ;
#14957=CARTESIAN_POINT ( 'NONE',  ( -0.2447605936724017717, 1.581084130983674951, -0.3379677220206969146 ) ) ;
#14959=CARTESIAN_POINT ( 'NONE',  ( 0.2249147617188371751, 1.559103846021539619, -0.3723417112827391295 ) ) ;
#14963=CARTESIAN_POINT ( 'NONE',  ( 0.1702344636782991416, 1.581111061277887808, -0.3809527529760087794 ) ) ;
#14969=DIRECTION ( 'NONE',  ( 0.000000000000000000, 0.000000000000000000, -1.000000000000000000 ) ) ;
#14971=DIRECTION ( 'NONE',  ( 0.000000000000000000, 0.000000000000000000, -1.000000000000000000 ) ) ;
#15007=VERTEX_POINT ( 'NONE', #5291 ) ;
#15030=ORIENTED_EDGE ( 'NONE', *, *, #3419, .F. ) ;
#15036=VECTOR ( 'NONE', #6429, 39.37007874015748143 ) ;
#15039=CARTESIAN_POINT ( 'NONE',  ( 0.000000000000000000, 1.239999999999999991, 0.000000000000000000 ) ) ;
#15048=CARTESIAN_POINT ( 'NONE',  ( 0.000000000000000000, 1.610000000000000098, 0.000000000000000000 ) ) ;
#15060=ORIENTED_EDGE ( 'NONE', *, *, #6754, .F. ) ;
#15061=CYLINDRICAL_SURFACE ( 'NONE', #14104, 0.4850000000000000422 ) ;
#15090=ORIENTED_EDGE ( 'NONE', *, *, #13537, .T. ) ;
#15100=CIRCLE ( 'NONE', #12411, 0.1068000000000000754 ) ;
#15103=VERTEX_POINT ( 'NONE', #3611 ) ;
#15104=AXIS2_PLACEMENT_3D ( 'NONE', #6513, #14610, #5442 ) ;
#15139=CIRCLE ( 'NONE', #8552, 0.3440000000000000280 ) ;
#15141=DIRECTION ( 'NONE',  ( -1.224646799147352961E-16, 0.000000000000000000, -1.000000000000000000 ) ) ;
#15193=COLOUR_RGB('Black',0.12,0.14,0.17);
#15194=FILL_AREA_STYLE_COLOUR('',#15193);
#15195=FILL_AREA_STYLE('',(#15194));
#15196=SURFACE_STYLE_FILL_AREA(#15195);
#15197=SURFACE_SIDE_STYLE('',(#15196));
#15198=SURFACE_STYLE_USAGE(.BOTH.,#15197);
#15199=PRESENTATION_STYLE_ASSIGNMENT((#15198));
ENDSEC;
END-ISO-10303-21;
